ISO-10303-21;
HEADER;
FILE_DESCRIPTION (('STEP AP214'),
    '1' );
FILE_NAME ('1-Center Box.step',
    '2026-10-28T16:50:19',
    ( '' ),
    ( '' ),
    'SwSTEP 2.0',
    'SolidWorks 2024',
    '' );
FILE_SCHEMA (( 'AUTOMOTIVE_DESIGN' ));
ENDSEC;

DATA;
#1=DIRECTION ( 'NONE',  ( -0.7071067811865456854, 9.059701919605289623E-16, -0.7071067811865493491 ) ) ;
#24=DIRECTION ( 'NONE',  ( 0.7071067811865494601, 0.7071067811865455743, 0.000000000000000000 ) ) ;
#31=VERTEX_POINT ( 'NONE', #8796 ) ;
#39=AXIS2_PLACEMENT_3D ( 'NONE', #7750, #9043, #8374 ) ;
#40=CARTESIAN_POINT ( 'NONE',  ( 29.50000000000000711, -29.99999999999996447, 2.500000000000015543 ) ) ;
#50=FACE_OUTER_BOUND ( 'NONE', #5817, .T. ) ;
#52=ORIENTED_EDGE ( 'NONE', *, *, #8438, .F. ) ;
#57=CARTESIAN_POINT ( 'NONE',  ( 29.50000000000000711, -32.49999999999997868, 58.99999999999997158 ) ) ;
#60=ADVANCED_FACE ( 'NONE', ( #7941 ), #7013, .F. ) ;
#61=DIRECTION ( 'NONE',  ( 1.000000000000000000, 0.000000000000000000, 0.000000000000000000 ) ) ;
#77=CARTESIAN_POINT ( 'NONE',  ( -4.703319286132082055, 17.49999999999999645, 14.50000000000000178 ) ) ;
#78=ADVANCED_FACE ( 'NONE', ( #8660 ), #4237, .F. ) ;
#81=DIRECTION ( 'NONE',  ( 0.000000000000000000, 0.000000000000000000, -1.000000000000000000 ) ) ;
#91=DIRECTION ( 'NONE',  ( -0.000000000000000000, -1.000000000000000000, -0.000000000000000000 ) ) ;
#99=LINE ( 'NONE', #8746, #418 ) ;
#104=EDGE_CURVE ( 'NONE', #1161, #4913, #2730, .T. ) ;
#111=CARTESIAN_POINT ( 'NONE',  ( 19.62310601229373930, -19.62310601229373930, 26.87436867076458924 ) ) ;
#120=ORIENTED_EDGE ( 'NONE', *, *, #516, .T. ) ;
#124=ORIENTED_EDGE ( 'NONE', *, *, #9169, .F. ) ;
#130=AXIS2_PLACEMENT_3D ( 'NONE', #2864, #5798, #1268 ) ;
#131=CARTESIAN_POINT ( 'NONE',  ( 27.00000000000000355, -29.99999999999999289, 64.00000000000000000 ) ) ;
#140=VECTOR ( 'NONE', #6903, 1000.000000000000000 ) ;
#157=DIRECTION ( 'NONE',  ( 0.7071067811865456854, -0.7071067811865493491, 0.000000000000000000 ) ) ;
#161=CARTESIAN_POINT ( 'NONE',  ( 4.703319286132084720, 17.49999999999999645, 14.50000000000000178 ) ) ;
#169=DIRECTION ( 'NONE',  ( -1.000000000000000000, 0.000000000000000000, 0.000000000000000000 ) ) ;
#176=DIRECTION ( 'NONE',  ( 0.000000000000000000, -0.000000000000000000, 1.000000000000000000 ) ) ;
#184=EDGE_LOOP ( 'NONE', ( #3377, #2801, #2753, #2032 ) ) ;
#186=ORIENTED_EDGE ( 'NONE', *, *, #3069, .F. ) ;
#192=EDGE_CURVE ( 'NONE', #9088, #5210, #6690, .T. ) ;
#198=ORIENTED_EDGE ( 'NONE', *, *, #3586, .T. ) ;
#213=CARTESIAN_POINT ( 'NONE',  ( -26.99999999999998934, 0.000000000000000000, 64.00000000000000000 ) ) ;
#217=ORIENTED_EDGE ( 'NONE', *, *, #4535, .F. ) ;
#218=AXIS2_PLACEMENT_3D ( 'NONE', #4359, #9398, #2914 ) ;
#219=ORIENTED_EDGE ( 'NONE', *, *, #9105, .T. ) ;
#221=CARTESIAN_POINT ( 'NONE',  ( -17.50000000000000355, 2.143131898507868643E-15, 0.000000000000000000 ) ) ;
#233=VERTEX_POINT ( 'NONE', #4579 ) ;
#235=DIRECTION ( 'NONE',  ( 0.7071067811865456854, -0.7071067811865493491, -0.000000000000000000 ) ) ;
#254=EDGE_LOOP ( 'NONE', ( #5839, #6022, #2019, #3735 ) ) ;
#256=ORIENTED_EDGE ( 'NONE', *, *, #3726, .F. ) ;
#265=ORIENTED_EDGE ( 'NONE', *, *, #8257, .F. ) ;
#267=ORIENTED_EDGE ( 'NONE', *, *, #4163, .F. ) ;
#270=CARTESIAN_POINT ( 'NONE',  ( -17.50000000000000355, 2.143131898507868643E-15, 49.50000000000000000 ) ) ;
#271=CARTESIAN_POINT ( 'NONE',  ( 0.000000000000000000, 34.00000000000001421, 32.00000000000000000 ) ) ;
#272=DIRECTION ( 'NONE',  ( 0.000000000000000000, 0.000000000000000000, 1.000000000000000000 ) ) ;
#274=DIRECTION ( 'NONE',  ( -0.7071067811865454633, 0.000000000000000000, -0.7071067811865494601 ) ) ;
#283=ORIENTED_EDGE ( 'NONE', *, *, #3869, .F. ) ;
#293=ORIENTED_EDGE ( 'NONE', *, *, #3069, .T. ) ;
#296=FACE_OUTER_BOUND ( 'NONE', #7526, .T. ) ;
#297=CARTESIAN_POINT ( 'NONE',  ( 12.37436867076458036, 12.37436867076458036, 44.37436867076458213 ) ) ;
#321=ORIENTED_EDGE ( 'NONE', *, *, #9216, .F. ) ;
#333=CARTESIAN_POINT ( 'NONE',  ( 0.000000000000000000, -17.50000000000000000, 49.50000000000000000 ) ) ;
#342=PLANE ( 'NONE',  #3730 ) ;
#347=DIRECTION ( 'NONE',  ( 0.000000000000000000, 0.000000000000000000, 1.000000000000000000 ) ) ;
#351=CARTESIAN_POINT ( 'NONE',  ( -26.99999999999998934, 35.00000000000000000, 5.000000000000004441 ) ) ;
#352=DIRECTION ( 'NONE',  ( 0.000000000000000000, -1.000000000000000000, 0.000000000000000000 ) ) ;
#359=LINE ( 'NONE', #3288, #3084 ) ;
#378=ORIENTED_EDGE ( 'NONE', *, *, #8438, .T. ) ;
#381=AXIS2_PLACEMENT_3D ( 'NONE', #4618, #6925, #3129 ) ;
#388=( BOUNDED_CURVE ( )  B_SPLINE_CURVE ( 3, ( #3943, #6883, #7691, #297 ),
 .UNSPECIFIED., .F., .T. ) 
 B_SPLINE_CURVE_WITH_KNOTS ( ( 4, 4 ),
 ( 0.000000000000000000, 0.7853981633974483900 ),
 .UNSPECIFIED. ) 
 CURVE ( )  GEOMETRIC_REPRESENTATION_ITEM ( )  RATIONAL_B_SPLINE_CURVE ( ( 1.000000000000000000, 0.9492530216741911220, 0.9492530216741911220, 1.000000000000000000 ) ) 
 REPRESENTATION_ITEM ( '' )  );
#397=ORIENTED_EDGE ( 'NONE', *, *, #2413, .T. ) ;
#402=DIRECTION ( 'NONE',  ( -1.000000000000000000, 0.000000000000000000, 0.000000000000000000 ) ) ;
#405=CARTESIAN_POINT ( 'NONE',  ( -17.50000000000000355, 2.143131898507868643E-15, 49.50000000000000000 ) ) ;
#412=ORIENTED_EDGE ( 'NONE', *, *, #8365, .F. ) ;
#414=AXIS2_PLACEMENT_3D ( 'NONE', #5872, #8891, #919 ) ;
#418=VECTOR ( 'NONE', #675, 1000.000000000000000 ) ;
#421=LINE ( 'NONE', #3354, #4265 ) ;
#428=VECTOR ( 'NONE', #1377, 1000.000000000000000 ) ;
#433=CARTESIAN_POINT ( 'NONE',  ( 12.37436867076458036, -12.37436867076458036, 19.62563132923542142 ) ) ;
#436=CARTESIAN_POINT ( 'NONE',  ( -12.37436867076458036, 12.37436867076458036, 19.62563132923542142 ) ) ;
#443=CARTESIAN_POINT ( 'NONE',  ( 31.00000000000002132, 0.000000000000000000, 32.00000000000000000 ) ) ;
#454=DIRECTION ( 'NONE',  ( 0.000000000000000000, 1.000000000000000000, 0.000000000000000000 ) ) ;
#459=ORIENTED_EDGE ( 'NONE', *, *, #6511, .F. ) ;
#461=ORIENTED_EDGE ( 'NONE', *, *, #4475, .T. ) ;
#463=LINE ( 'NONE', #6333, #3982 ) ;
#466=DIRECTION ( 'NONE',  ( -0.5773502691896283956, 0.5773502691896229555, 0.5773502691896260641 ) ) ;
#469=CONICAL_SURFACE ( 'NONE', #1852, 18.49999999999998934, 0.7853981633974517207 ) ;
#474=EDGE_CURVE ( 'NONE', #1673, #5235, #848, .T. ) ;
#479=EDGE_LOOP ( 'NONE', ( #8954, #2273 ) ) ;
#493=ORIENTED_EDGE ( 'NONE', *, *, #6896, .F. ) ;
#502=ORIENTED_EDGE ( 'NONE', *, *, #6422, .F. ) ;
#516=EDGE_CURVE ( 'NONE', #1904, #3854, #5179, .T. ) ;
#535=EDGE_CURVE ( 'NONE', #3097, #7881, #1674, .T. ) ;
#543=CARTESIAN_POINT ( 'NONE',  ( -17.50000000000000355, 2.143131898507868643E-15, 14.49999999999999822 ) ) ;
#569=DIRECTION ( 'NONE',  ( -0.000000000000000000, 1.000000000000000000, -0.000000000000000000 ) ) ;
#573=CARTESIAN_POINT ( 'NONE',  ( -26.99999999999998934, 29.99999999999997158, 64.00000000000000000 ) ) ;
#579=AXIS2_PLACEMENT_3D ( 'NONE', #3294, #9015, #8255 ) ;
#590=DIRECTION ( 'NONE',  ( 0.7071067811865490160, -0.7071067811865461294, 0.000000000000000000 ) ) ;
#593=CARTESIAN_POINT ( 'NONE',  ( 32.00000000000000711, 29.99999999999997868, 64.00000000000000000 ) ) ;
#600=CARTESIAN_POINT ( 'NONE',  ( 32.00000000000000711, -29.99999999999996447, 58.99999999999997158 ) ) ;
#608=EDGE_CURVE ( 'NONE', #8189, #5235, #3253, .T. ) ;
#622=CARTESIAN_POINT ( 'NONE',  ( 12.37436867076458036, -12.37436867076458036, 19.62563132923542142 ) ) ;
#628=ORIENTED_EDGE ( 'NONE', *, *, #7466, .T. ) ;
#638=VECTOR ( 'NONE', #352, 1000.000000000000000 ) ;
#642=( BOUNDED_CURVE ( )  B_SPLINE_CURVE ( 3, ( #1543, #1590, #161, #2983 ),
 .UNSPECIFIED., .F., .T. ) 
 B_SPLINE_CURVE_WITH_KNOTS ( ( 4, 4 ),
 ( 2.356194490192344837, 3.141592653589793116 ),
 .UNSPECIFIED. ) 
 CURVE ( )  GEOMETRIC_REPRESENTATION_ITEM ( )  RATIONAL_B_SPLINE_CURVE ( ( 1.000000000000000000, 0.9492530216741911220, 0.9492530216741911220, 1.000000000000000000 ) ) 
 REPRESENTATION_ITEM ( '' )  );
#644=CARTESIAN_POINT ( 'NONE',  ( 27.00000000000000355, -34.99999999999999289, 5.000000000000004441 ) ) ;
#647=ORIENTED_EDGE ( 'NONE', *, *, #2998, .F. ) ;
#652=LINE ( 'NONE', #6703, #1819 ) ;
#660=ADVANCED_FACE ( 'NONE', ( #8624 ), #2088, .F. ) ;
#668=ORIENTED_EDGE ( 'NONE', *, *, #3534, .T. ) ;
#673=CONICAL_SURFACE ( 'NONE', #7266, 18.50000000000001776, 0.7853981633974431720 ) ;
#675=DIRECTION ( 'NONE',  ( 0.000000000000000000, 0.000000000000000000, -1.000000000000000000 ) ) ;
#705=AXIS2_PLACEMENT_3D ( 'NONE', #1183, #466, #3392 ) ;
#723=CARTESIAN_POINT ( 'NONE',  ( 0.000000000000000000, 0.000000000000000000, 0.000000000000000000 ) ) ;
#737=CARTESIAN_POINT ( 'NONE',  ( 32.00000000000000711, -34.99999999999999289, 5.000000000000004441 ) ) ;
#752=CARTESIAN_POINT ( 'NONE',  ( -31.99999999999999289, -29.99999999999996447, 5.000000000000004441 ) ) ;
#758=EDGE_CURVE ( 'NONE', #2331, #2908, #463, .T. ) ;
#759=CARTESIAN_POINT ( 'NONE',  ( -31.99999999999999289, -29.99999999999996447, 5.000000000000004441 ) ) ;
#761=DIRECTION ( 'NONE',  ( 0.000000000000000000, 0.000000000000000000, -1.000000000000000000 ) ) ;
#771=FACE_OUTER_BOUND ( 'NONE', #4073, .T. ) ;
#783=ORIENTED_EDGE ( 'NONE', *, *, #2600, .T. ) ;
#791=CARTESIAN_POINT ( 'NONE',  ( 0.000000000000000000, -35.00000000000000000, 32.00000000000000000 ) ) ;
#794=VERTEX_POINT ( 'NONE', #8808 ) ;
#797=EDGE_LOOP ( 'NONE', ( #9401, #3064, #5815, #6633, #7802, #2283, #3467 ) ) ;
#798=CONICAL_SURFACE ( 'NONE', #4334, 17.50000000000000355, 0.7853981633974533860 ) ;
#816=DIRECTION ( 'NONE',  ( 1.000000000000000000, -0.000000000000000000, -0.000000000000000000 ) ) ;
#819=ORIENTED_EDGE ( 'NONE', *, *, #104, .F. ) ;
#822=LINE ( 'NONE', #3762, #9334 ) ;
#826=FACE_OUTER_BOUND ( 'NONE', #3541, .T. ) ;
#831=ORIENTED_EDGE ( 'NONE', *, *, #3103, .T. ) ;
#842=FACE_OUTER_BOUND ( 'NONE', #1082, .T. ) ;
#848=LINE ( 'NONE', #1473, #9157 ) ;
#861=AXIS2_PLACEMENT_3D ( 'NONE', #9190, #3916, #1078 ) ;
#872=ORIENTED_EDGE ( 'NONE', *, *, #5714, .F. ) ;
#873=VECTOR ( 'NONE', #816, 1000.000000000000000 ) ;
#884=AXIS2_PLACEMENT_3D ( 'NONE', #8973, #2356, #3934 ) ;
#885=ORIENTED_EDGE ( 'NONE', *, *, #3309, .F. ) ;
#886=ORIENTED_EDGE ( 'NONE', *, *, #3534, .F. ) ;
#895=EDGE_CURVE ( 'NONE', #4382, #1673, #652, .T. ) ;
#909=CARTESIAN_POINT ( 'NONE',  ( 17.50000000000000355, 0.000000000000000000, 14.49999999999999822 ) ) ;
#918=FACE_OUTER_BOUND ( 'NONE', #5596, .T. ) ;
#919=DIRECTION ( 'NONE',  ( 0.000000000000000000, 0.000000000000000000, 1.000000000000000000 ) ) ;
#921=ORIENTED_EDGE ( 'NONE', *, *, #3528, .F. ) ;
#967=ORIENTED_EDGE ( 'NONE', *, *, #4663, .T. ) ;
#977=ORIENTED_EDGE ( 'NONE', *, *, #758, .F. ) ;
#980=CARTESIAN_POINT ( 'NONE',  ( 27.00000000000000355, 0.000000000000000000, 64.00000000000000000 ) ) ;
#981=FACE_OUTER_BOUND ( 'NONE', #4924, .T. ) ;
#1001=EDGE_LOOP ( 'NONE', ( #5875, #1692, #2814, #3013 ) ) ;
#1005=( BOUNDED_CURVE ( )  B_SPLINE_CURVE ( 3, ( #543, #9331, #4964, #1942 ),
 .UNSPECIFIED., .F., .F. ) 
 B_SPLINE_CURVE_WITH_KNOTS ( ( 4, 4 ),
 ( 3.141592653589793116, 3.926990816987241395 ),
 .UNSPECIFIED. ) 
 CURVE ( )  GEOMETRIC_REPRESENTATION_ITEM ( )  RATIONAL_B_SPLINE_CURVE ( ( 1.000000000000000000, 0.9492530216741911220, 0.9492530216741911220, 1.000000000000000000 ) ) 
 REPRESENTATION_ITEM ( '' )  );
#1007=EDGE_CURVE ( 'NONE', #6890, #1286, #5367, .T. ) ;
#1010=FACE_OUTER_BOUND ( 'NONE', #6789, .T. ) ;
#1019=DIRECTION ( 'NONE',  ( 0.000000000000000000, -1.000000000000000000, 0.000000000000000000 ) ) ;
#1038=AXIS2_PLACEMENT_3D ( 'NONE', #8823, #5176, #4791 ) ;
#1043=EDGE_LOOP ( 'NONE', ( #4538, #3271, #886 ) ) ;
#1045=LINE ( 'NONE', #6153, #3192 ) ;
#1052=ORIENTED_EDGE ( 'NONE', *, *, #5118, .T. ) ;
#1058=CARTESIAN_POINT ( 'NONE',  ( 0.000000000000000000, 29.99999999999997158, 64.00000000000000000 ) ) ;
#1064=ORIENTED_EDGE ( 'NONE', *, *, #6422, .T. ) ;
#1069=PLANE ( 'NONE',  #2288 ) ;
#1078=DIRECTION ( 'NONE',  ( 0.000000000000000000, 0.000000000000000000, 1.000000000000000000 ) ) ;
#1082=EDGE_LOOP ( 'NONE', ( #2203, #6488, #5793, #3396, #2394, #6109 ) ) ;
#1085=ORIENTED_EDGE ( 'NONE', *, *, #4803, .F. ) ;
#1095=EDGE_CURVE ( 'NONE', #6009, #3216, #4282, .T. ) ;
#1100=ADVANCED_FACE ( 'NONE', ( #771 ), #5823, .F. ) ;
#1120=CARTESIAN_POINT ( 'NONE',  ( 27.00000000000000355, 29.99999999999997158, 0.000000000000000000 ) ) ;
#1122=CARTESIAN_POINT ( 'NONE',  ( -17.50000000000000355, 2.143131898507868643E-15, 0.000000000000000000 ) ) ;
#1127=VECTOR ( 'NONE', #3429, 1000.000000000000000 ) ;
#1137=FACE_OUTER_BOUND ( 'NONE', #1043, .T. ) ;
#1138=DIRECTION ( 'NONE',  ( 0.7071067811865439090, 8.659560562354979697E-17, 0.7071067811865512365 ) ) ;
#1158=DIRECTION ( 'NONE',  ( -0.5773502691896251759, 0.5773502691896228445, -0.5773502691896293948 ) ) ;
#1161=VERTEX_POINT ( 'NONE', #3034 ) ;
#1163=VERTEX_POINT ( 'NONE', #7258 ) ;
#1167=DIRECTION ( 'NONE',  ( 0.000000000000000000, 0.7071067811865455743, -0.7071067811865494601 ) ) ;
#1183=CARTESIAN_POINT ( 'NONE',  ( -31.99999999999999289, 29.99999999999997868, 58.99999999999997158 ) ) ;
#1184=FACE_OUTER_BOUND ( 'NONE', #3778, .T. ) ;
#1193=ORIENTED_EDGE ( 'NONE', *, *, #4803, .T. ) ;
#1195=( GEOMETRIC_REPRESENTATION_CONTEXT ( 3 ) GLOBAL_UNCERTAINTY_ASSIGNED_CONTEXT ( ( #3839 ) ) GLOBAL_UNIT_ASSIGNED_CONTEXT ( ( #5393, #3130, #5485 ) ) REPRESENTATION_CONTEXT ( 'NONE', 'WORKASPACE' ) );
#1203=AXIS2_PLACEMENT_3D ( 'NONE', #351, #1158, #6796 ) ;
#1209=CARTESIAN_POINT ( 'NONE',  ( 2.265596578422601819E-15, -34.99999999999999289, 50.49999999999998579 ) ) ;
#1212=( NAMED_UNIT ( * ) SI_UNIT ( $, .STERADIAN. ) SOLID_ANGLE_UNIT ( ) );
#1218=EDGE_CURVE ( 'NONE', #9088, #8254, #2902, .T. ) ;
#1220=EDGE_LOOP ( 'NONE', ( #628, #4675, #1579 ) ) ;
#1221=EDGE_LOOP ( 'NONE', ( #2803, #124, #783, #1287 ) ) ;
#1238=DIRECTION ( 'NONE',  ( 8.659560562354994488E-17, 0.7071067811865426878, -0.7071067811865524577 ) ) ;
#1242=ORIENTED_EDGE ( 'NONE', *, *, #3296, .F. ) ;
#1253=ADVANCED_FACE ( 'NONE', ( #918 ), #7189, .F. ) ;
#1263=EDGE_LOOP ( 'NONE', ( #1622, #2699, #2434, #819, #7270, #3505 ) ) ;
#1268=DIRECTION ( 'NONE',  ( 0.000000000000000000, 0.000000000000000000, 1.000000000000000000 ) ) ;
#1279=DIRECTION ( 'NONE',  ( 0.000000000000000000, 0.000000000000000000, 1.000000000000000000 ) ) ;
#1286=VERTEX_POINT ( 'NONE', #6928 ) ;
#1287=ORIENTED_EDGE ( 'NONE', *, *, #1925, .F. ) ;
#1294=EDGE_CURVE ( 'NONE', #9088, #1890, #5486, .T. ) ;
#1295=APPLICATION_CONTEXT ( 'automotive_design' ) ;
#1297=AXIS2_PLACEMENT_3D ( 'NONE', #3610, #8890, #1641 ) ;
#1307=( BOUNDED_CURVE ( )  B_SPLINE_CURVE ( 3, ( #333, #1628, #3887, #4756 ),
 .UNSPECIFIED., .F., .T. ) 
 B_SPLINE_CURVE_WITH_KNOTS ( ( 4, 4 ),
 ( 0.000000000000000000, 0.7853981633974483900 ),
 .UNSPECIFIED. ) 
 CURVE ( )  GEOMETRIC_REPRESENTATION_ITEM ( )  RATIONAL_B_SPLINE_CURVE ( ( 1.000000000000000000, 0.9492530216741911220, 0.9492530216741911220, 1.000000000000000000 ) ) 
 REPRESENTATION_ITEM ( '' )  );
#1317=ORIENTED_EDGE ( 'NONE', *, *, #2600, .F. ) ;
#1329=ORIENTED_EDGE ( 'NONE', *, *, #8935, .F. ) ;
#1332=VECTOR ( 'NONE', #4765, 1000.000000000000000 ) ;
#1352=VECTOR ( 'NONE', #9344, 1000.000000000000114 ) ;
#1355=DIRECTION ( 'NONE',  ( 0.000000000000000000, 0.000000000000000000, -1.000000000000000000 ) ) ;
#1370=DIRECTION ( 'NONE',  ( 0.7071067811865493491, -1.126022036214515194E-15, -0.7071067811865455743 ) ) ;
#1371=( BOUNDED_CURVE ( )  B_SPLINE_CURVE ( 3, ( #7360, #8712, #111, #2172 ),
 .UNSPECIFIED., .F., .T. ) 
 B_SPLINE_CURVE_WITH_KNOTS ( ( 4, 4 ),
 ( 2.356194490192345281, 3.926990816987240951 ),
 .UNSPECIFIED. ) 
 CURVE ( )  GEOMETRIC_REPRESENTATION_ITEM ( )  RATIONAL_B_SPLINE_CURVE ( ( 1.000000000000000000, 0.8047378541243652705, 0.8047378541243652705, 1.000000000000000000 ) ) 
 REPRESENTATION_ITEM ( '' )  );
#1374=FACE_OUTER_BOUND ( 'NONE', #2741, .T. ) ;
#1377=DIRECTION ( 'NONE',  ( -1.000000000000000000, 0.000000000000000000, 0.000000000000000000 ) ) ;
#1386=EDGE_LOOP ( 'NONE', ( #9060, #4980, #3350 ) ) ;
#1390=ORIENTED_EDGE ( 'NONE', *, *, #7995, .T. ) ;
#1392=DIRECTION ( 'NONE',  ( -1.000000000000000000, 0.000000000000000000, 0.000000000000000000 ) ) ;
#1417=ADVANCED_FACE ( 'NONE', ( #3499 ), #6448, .T. ) ;
#1418=EDGE_CURVE ( 'NONE', #7789, #3651, #3022, .T. ) ;
#1421=DIRECTION ( 'NONE',  ( 0.000000000000000000, 0.000000000000000000, 1.000000000000000000 ) ) ;
#1432=DIRECTION ( 'NONE',  ( 1.000000000000000000, 0.000000000000000000, 0.000000000000000000 ) ) ;
#1452=DIRECTION ( 'NONE',  ( 0.000000000000000000, 0.000000000000000000, 1.000000000000000000 ) ) ;
#1470=ORIENTED_EDGE ( 'NONE', *, *, #8299, .T. ) ;
#1473=CARTESIAN_POINT ( 'NONE',  ( 27.00000000000000355, 35.00000000000000000, 64.00000000000000000 ) ) ;
#1474=FACE_OUTER_BOUND ( 'NONE', #2115, .T. ) ;
#1482=ORIENTED_EDGE ( 'NONE', *, *, #1551, .T. ) ;
#1494=DIRECTION ( 'NONE',  ( 0.000000000000000000, 0.000000000000000000, -1.000000000000000000 ) ) ;
#1498=DIRECTION ( 'NONE',  ( -1.000000000000000000, -0.000000000000000000, -0.000000000000000000 ) ) ;
#1505=CARTESIAN_POINT ( 'NONE',  ( -9.048619709455117288, 15.70011763207404520, 47.70011763207404698 ) ) ;
#1515=AXIS2_PLACEMENT_3D ( 'NONE', #6650, #3043, #3811 ) ;
#1526=LINE ( 'NONE', #7385, #5346 ) ;
#1543=CARTESIAN_POINT ( 'NONE',  ( 12.37436867076458036, 12.37436867076458036, 19.62563132923542142 ) ) ;
#1544=CIRCLE ( 'NONE', #6922, 18.50000000000000355 ) ;
#1551=EDGE_CURVE ( 'NONE', #3216, #6009, #2254, .T. ) ;
#1553=CARTESIAN_POINT ( 'NONE',  ( -4.703319286132082944, 17.49999999999999645, 49.50000000000000000 ) ) ;
#1566=CARTESIAN_POINT ( 'NONE',  ( -9.048619709455111959, -15.70011763207404876, 16.29988236792595302 ) ) ;
#1570=ORIENTED_EDGE ( 'NONE', *, *, #7422, .T. ) ;
#1574=AXIS2_PLACEMENT_3D ( 'NONE', #6606, #24, #5876 ) ;
#1579=ORIENTED_EDGE ( 'NONE', *, *, #9105, .F. ) ;
#1584=DIRECTION ( 'NONE',  ( 1.000000000000000000, 0.000000000000000000, 0.000000000000000000 ) ) ;
#1590=CARTESIAN_POINT ( 'NONE',  ( 9.048619709455111959, 15.70011763207404876, 16.29988236792595302 ) ) ;
#1601=CARTESIAN_POINT ( 'NONE',  ( -15.70011763207405231, 9.048619709455117288, 47.70011763207405409 ) ) ;
#1613=CARTESIAN_POINT ( 'NONE',  ( 19.62310601229373930, 19.62310601229373930, 26.87436867076457503 ) ) ;
#1614=AXIS2_PLACEMENT_3D ( 'NONE', #6760, #5504, #4539 ) ;
#1622=ORIENTED_EDGE ( 'NONE', *, *, #1720, .F. ) ;
#1626=CARTESIAN_POINT ( 'NONE',  ( -18.50000000000001776, 0.000000000000000000, 0.000000000000000000 ) ) ;
#1627=UNCERTAINTY_MEASURE_WITH_UNIT (LENGTH_MEASURE( 1.000000000000000082E-05 ), #4150, 'distance_accuracy_value', 'NONE');
#1628=CARTESIAN_POINT ( 'NONE',  ( -4.703319286132083832, -17.49999999999999645, 49.50000000000000000 ) ) ;
#1632=SHAPE_DEFINITION_REPRESENTATION ( #8161, #3963 ) ;
#1641=DIRECTION ( 'NONE',  ( 0.000000000000000000, 0.000000000000000000, -1.000000000000000000 ) ) ;
#1654=DIRECTION ( 'NONE',  ( 0.000000000000000000, 0.000000000000000000, -1.000000000000000000 ) ) ;
#1661=EDGE_CURVE ( 'NONE', #7899, #5896, #1307, .T. ) ;
#1662=DIRECTION ( 'NONE',  ( 0.000000000000000000, 1.000000000000000000, 0.000000000000000000 ) ) ;
#1673=VERTEX_POINT ( 'NONE', #6107 ) ;
#1674=LINE ( 'NONE', #6866, #6200 ) ;
#1676=CARTESIAN_POINT ( 'NONE',  ( 17.49999999999999645, 4.703319286132083832, 49.50000000000000000 ) ) ;
#1687=( BOUNDED_CURVE ( )  B_SPLINE_CURVE ( 3, ( #5215, #77, #2999, #5935 ),
 .UNSPECIFIED., .F., .T. ) 
 B_SPLINE_CURVE_WITH_KNOTS ( ( 4, 4 ),
 ( 3.141592653589793116, 3.926990816987241395 ),
 .UNSPECIFIED. ) 
 CURVE ( )  GEOMETRIC_REPRESENTATION_ITEM ( )  RATIONAL_B_SPLINE_CURVE ( ( 1.000000000000000000, 0.9492530216741911220, 0.9492530216741911220, 1.000000000000000000 ) ) 
 REPRESENTATION_ITEM ( '' )  );
#1692=ORIENTED_EDGE ( 'NONE', *, *, #6006, .F. ) ;
#1694=VERTEX_POINT ( 'NONE', #909 ) ;
#1696=CARTESIAN_POINT ( 'NONE',  ( 0.000000000000000000, 0.000000000000000000, 63.00000000000002842 ) ) ;
#1697=DIRECTION ( 'NONE',  ( -1.000000000000000000, 0.000000000000000000, 0.000000000000000000 ) ) ;
#1699=VERTEX_POINT ( 'NONE', #6966 ) ;
#1703=ADVANCED_FACE ( 'NONE', ( #8926 ), #4705, .T. ) ;
#1705=DIRECTION ( 'NONE',  ( 1.000000000000000000, -0.000000000000000000, -0.000000000000000000 ) ) ;
#1719=EDGE_CURVE ( 'NONE', #4290, #7899, #6237, .T. ) ;
#1720=EDGE_CURVE ( 'NONE', #3965, #6890, #421, .T. ) ;
#1721=ORIENTED_EDGE ( 'NONE', *, *, #9169, .T. ) ;
#1727=EDGE_LOOP ( 'NONE', ( #8694, #283, #6075, #2298 ) ) ;
#1731=EDGE_CURVE ( 'NONE', #7912, #7789, #3395, .T. ) ;
#1746=ORIENTED_EDGE ( 'NONE', *, *, #3218, .T. ) ;
#1750=LINE ( 'NONE', #980, #8019 ) ;
#1779=DIRECTION ( 'NONE',  ( 0.000000000000000000, 0.000000000000000000, 1.000000000000000000 ) ) ;
#1797=CARTESIAN_POINT ( 'NONE',  ( 17.50000000000000355, 0.000000000000000000, 63.00000000000002842 ) ) ;
#1812=DIRECTION ( 'NONE',  ( -0.7071067811865460184, -0.7071067811865489050, -9.185433182841358520E-17 ) ) ;
#1819=VECTOR ( 'NONE', #8768, 1000.000000000000000 ) ;
#1823=ORIENTED_EDGE ( 'NONE', *, *, #3528, .T. ) ;
#1827=PLANE ( 'NONE',  #381 ) ;
#1838=EDGE_CURVE ( 'NONE', #2635, #2331, #2095, .T. ) ;
#1841=CARTESIAN_POINT ( 'NONE',  ( 32.00000000000000711, -34.99999999999999289, 64.00000000000000000 ) ) ;
#1849=CARTESIAN_POINT ( 'NONE',  ( -17.50000000000000355, 2.143131898507868643E-15, 63.00000000000002842 ) ) ;
#1852=AXIS2_PLACEMENT_3D ( 'NONE', #7055, #2684, #3393 ) ;
#1863=CARTESIAN_POINT ( 'NONE',  ( 27.00000000000000355, 35.00000000000000000, 59.00000000000000000 ) ) ;
#1866=CARTESIAN_POINT ( 'NONE',  ( -26.99999999999998934, -34.99999999999999289, 5.000000000000004441 ) ) ;
#1877=DIRECTION ( 'NONE',  ( 0.000000000000000000, 0.000000000000000000, -1.000000000000000000 ) ) ;
#1885=CYLINDRICAL_SURFACE ( 'NONE', #2072, 17.50000000000000000 ) ;
#1886=LINE ( 'NONE', #6317, #638 ) ;
#1890=VERTEX_POINT ( 'NONE', #8775 ) ;
#1904=VERTEX_POINT ( 'NONE', #6482 ) ;
#1914=DIRECTION ( 'NONE',  ( 0.000000000000000000, 0.000000000000000000, 1.000000000000000000 ) ) ;
#1922=DIRECTION ( 'NONE',  ( 1.000000000000000000, 0.000000000000000000, 0.000000000000000000 ) ) ;
#1923=DIRECTION ( 'NONE',  ( -0.7071067811865494601, 0.000000000000000000, -0.7071067811865455743 ) ) ;
#1924=ORIENTED_EDGE ( 'NONE', *, *, #1294, .T. ) ;
#1925=EDGE_CURVE ( 'NONE', #8795, #9218, #5033, .T. ) ;
#1931=ADVANCED_FACE ( 'NONE', ( #2825 ), #7331, .T. ) ;
#1934=CYLINDRICAL_SURFACE ( 'NONE', #2171, 17.50000000000000355 ) ;
#1936=ORIENTED_EDGE ( 'NONE', *, *, #6947, .T. ) ;
#1942=CARTESIAN_POINT ( 'NONE',  ( -12.37436867076458036, -12.37436867076458036, 19.62563132923542142 ) ) ;
#1953=ORIENTED_EDGE ( 'NONE', *, *, #3230, .T. ) ;
#1981=APPLICATION_CONTEXT ( 'automotive_design' ) ;
#1992=( BOUNDED_CURVE ( )  B_SPLINE_CURVE ( 3, ( #433, #6307, #6346, #4277 ),
 .UNSPECIFIED., .F., .T. ) 
 B_SPLINE_CURVE_WITH_KNOTS ( ( 4, 4 ),
 ( 2.356194490192344837, 3.141592653589793116 ),
 .UNSPECIFIED. ) 
 CURVE ( )  GEOMETRIC_REPRESENTATION_ITEM ( )  RATIONAL_B_SPLINE_CURVE ( ( 1.000000000000000000, 0.9492530216741911220, 0.9492530216741911220, 1.000000000000000000 ) ) 
 REPRESENTATION_ITEM ( '' )  );
#1995=DIRECTION ( 'NONE',  ( 0.000000000000000000, 0.000000000000000000, 1.000000000000000000 ) ) ;
#2001=LINE ( 'NONE', #5889, #6430 ) ;
#2003=PLANE ( 'NONE',  #6616 ) ;
#2017=CARTESIAN_POINT ( 'NONE',  ( 31.00000000000002132, 0.000000000000000000, 32.00000000000000000 ) ) ;
#2019=ORIENTED_EDGE ( 'NONE', *, *, #4534, .T. ) ;
#2020=ORIENTED_EDGE ( 'NONE', *, *, #4070, .F. ) ;
#2024=CARTESIAN_POINT ( 'NONE',  ( 32.00000000000000711, -34.99999999999999289, 58.99999999999997158 ) ) ;
#2025=AXIS2_PLACEMENT_3D ( 'NONE', #7303, #61, #3752 ) ;
#2032=ORIENTED_EDGE ( 'NONE', *, *, #474, .T. ) ;
#2039=CARTESIAN_POINT ( 'NONE',  ( -31.99999999999999289, 29.99999999999997868, 58.99999999999997158 ) ) ;
#2041=EDGE_LOOP ( 'NONE', ( #921, #321, #1193, #6734 ) ) ;
#2043=ORIENTED_EDGE ( 'NONE', *, *, #5760, .T. ) ;
#2047=CARTESIAN_POINT ( 'NONE',  ( 0.000000000000000000, 0.000000000000000000, 0.000000000000000000 ) ) ;
#2061=VECTOR ( 'NONE', #6374, 1000.000000000000114 ) ;
#2065=ORIENTED_EDGE ( 'NONE', *, *, #3292, .T. ) ;
#2066=ORIENTED_EDGE ( 'NONE', *, *, #1719, .F. ) ;
#2072=AXIS2_PLACEMENT_3D ( 'NONE', #2614, #5545, #8470 ) ;
#2074=DIRECTION ( 'NONE',  ( -0.000000000000000000, -0.000000000000000000, 1.000000000000000000 ) ) ;
#2088=CYLINDRICAL_SURFACE ( 'NONE', #3504, 17.50000000000000355 ) ;
#2095=LINE ( 'NONE', #3008, #428 ) ;
#2109=VECTOR ( 'NONE', #5620, 1000.000000000000000 ) ;
#2115=EDGE_LOOP ( 'NONE', ( #2547, #6798, #831, #4788, #4948, #397 ) ) ;
#2117=AXIS2_PLACEMENT_3D ( 'NONE', #4837, #7817, #2818 ) ;
#2119=CARTESIAN_POINT ( 'NONE',  ( -31.99999999999999289, 0.000000000000000000, 50.50000000000001421 ) ) ;
#2122=PLANE ( 'NONE',  #9006 ) ;
#2128=ADVANCED_FACE ( 'NONE', ( #4157 ), #5280, .F. ) ;
#2129=ORIENTED_EDGE ( 'NONE', *, *, #535, .F. ) ;
#2137=EDGE_CURVE ( 'NONE', #6770, #2908, #6423, .T. ) ;
#2139=ORIENTED_EDGE ( 'NONE', *, *, #9357, .T. ) ;
#2142=DIRECTION ( 'NONE',  ( 9.614813431917774709E-17, 0.7071067811865493491, -0.7071067811865455743 ) ) ;
#2164=DIRECTION ( 'NONE',  ( 0.000000000000000000, 0.000000000000000000, -1.000000000000000000 ) ) ;
#2171=AXIS2_PLACEMENT_3D ( 'NONE', #2891, #2074, #7796 ) ;
#2172=CARTESIAN_POINT ( 'NONE',  ( 12.37436867076458036, -12.37436867076458036, 19.62563132923542142 ) ) ;
#2174=LINE ( 'NONE', #7313, #2454 ) ;
#2177=EDGE_CURVE ( 'NONE', #1699, #4010, #3290, .T. ) ;
#2181=VECTOR ( 'NONE', #347, 1000.000000000000000 ) ;
#2191=EDGE_CURVE ( 'NONE', #5210, #4201, #4664, .T. ) ;
#2192=CARTESIAN_POINT ( 'NONE',  ( 0.000000000000000000, 34.00000000000001421, 32.00000000000000000 ) ) ;
#2197=FACE_OUTER_BOUND ( 'NONE', #5985, .T. ) ;
#2203=ORIENTED_EDGE ( 'NONE', *, *, #2322, .F. ) ;
#2249=EDGE_CURVE ( 'NONE', #8566, #9251, #5109, .T. ) ;
#2254=CIRCLE ( 'NONE', #4867, 18.50000000000001776 ) ;
#2273=ORIENTED_EDGE ( 'NONE', *, *, #1925, .T. ) ;
#2276=LINE ( 'NONE', #6029, #6897 ) ;
#2283=ORIENTED_EDGE ( 'NONE', *, *, #1719, .T. ) ;
#2287=DIRECTION ( 'NONE',  ( -0.000000000000000000, -0.000000000000000000, 1.000000000000000000 ) ) ;
#2288=AXIS2_PLACEMENT_3D ( 'NONE', #1841, #1697, #5498 ) ;
#2292=CARTESIAN_POINT ( 'NONE',  ( -12.37436867076458036, -12.37436867076458036, 44.37436867076458213 ) ) ;
#2294=VERTEX_POINT ( 'NONE', #600 ) ;
#2298=ORIENTED_EDGE ( 'NONE', *, *, #7347, .F. ) ;
#2302=( BOUNDED_CURVE ( )  B_SPLINE_CURVE ( 3, ( #8197, #1613, #3104, #5993 ),
 .UNSPECIFIED., .F., .F. ) 
 B_SPLINE_CURVE_WITH_KNOTS ( ( 4, 4 ),
 ( 5.497787143782137953, 7.068583470577034511 ),
 .UNSPECIFIED. ) 
 CURVE ( )  GEOMETRIC_REPRESENTATION_ITEM ( )  RATIONAL_B_SPLINE_CURVE ( ( 1.000000000000000000, 0.8047378541243649375, 0.8047378541243649375, 1.000000000000000000 ) ) 
 REPRESENTATION_ITEM ( '' )  );
#2307=PRODUCT_DEFINITION_CONTEXT ( 'detailed design', #1295, 'design' ) ;
#2321=CIRCLE ( 'NONE', #6003, 17.50000000000000000 ) ;
#2322=EDGE_CURVE ( 'NONE', #4035, #3697, #3803, .T. ) ;
#2331=VERTEX_POINT ( 'NONE', #4621 ) ;
#2341=STYLED_ITEM('',(#9515),#6309);
#2345=VECTOR ( 'NONE', #4771, 1000.000000000000114 ) ;
#2356=DIRECTION ( 'NONE',  ( 0.5773502691896290617, -0.5773502691896258421, 0.5773502691896225114 ) ) ;
#2358=ORIENTED_EDGE ( 'NONE', *, *, #3869, .T. ) ;
#2377=CARTESIAN_POINT ( 'NONE',  ( 0.000000000000000000, 34.00000000000001421, 49.50000000000000000 ) ) ;
#2383=ORIENTED_EDGE ( 'NONE', *, *, #3957, .T. ) ;
#2390=PLANE ( 'NONE',  #8661 ) ;
#2394=ORIENTED_EDGE ( 'NONE', *, *, #6421, .T. ) ;
#2407=ORIENTED_EDGE ( 'NONE', *, *, #3115, .F. ) ;
#2412=DIRECTION ( 'NONE',  ( 0.000000000000000000, 0.000000000000000000, -1.000000000000000000 ) ) ;
#2413=EDGE_CURVE ( 'NONE', #6515, #1161, #4879, .T. ) ;
#2432=ADVANCED_FACE ( 'NONE', ( #2510 ), #342, .F. ) ;
#2434=ORIENTED_EDGE ( 'NONE', *, *, #5104, .T. ) ;
#2441=VECTOR ( 'NONE', #235, 1000.000000000000114 ) ;
#2443=CARTESIAN_POINT ( 'NONE',  ( -12.37436867076458036, -12.37436867076458036, 19.62563132923542142 ) ) ;
#2454=VECTOR ( 'NONE', #3090, 1000.000000000000000 ) ;
#2456=CARTESIAN_POINT ( 'NONE',  ( 2.143131898507868248E-15, 34.00000000000001421, 14.49999999999999822 ) ) ;
#2461=VERTEX_POINT ( 'NONE', #4176 ) ;
#2494=ORIENTED_EDGE ( 'NONE', *, *, #5604, .F. ) ;
#2495=ADVANCED_FACE ( 'NONE', ( #4322 ), #3364, .T. ) ;
#2506=CARTESIAN_POINT ( 'NONE',  ( 15.70011763207405231, -9.048619709455117288, 47.70011763207405409 ) ) ;
#2510=FACE_OUTER_BOUND ( 'NONE', #1727, .T. ) ;
#2513=ORIENTED_EDGE ( 'NONE', *, *, #8827, .T. ) ;
#2514=CARTESIAN_POINT ( 'NONE',  ( 32.00000000000000711, 29.99999999999997868, 5.000000000000031974 ) ) ;
#2522=EDGE_CURVE ( 'NONE', #2562, #1694, #1992, .T. ) ;
#2529=LINE ( 'NONE', #1122, #8459 ) ;
#2539=DIRECTION ( 'NONE',  ( 0.000000000000000000, 1.000000000000000000, 0.000000000000000000 ) ) ;
#2541=ORIENTED_EDGE ( 'NONE', *, *, #2177, .T. ) ;
#2547=ORIENTED_EDGE ( 'NONE', *, *, #6826, .F. ) ;
#2562=VERTEX_POINT ( 'NONE', #622 ) ;
#2567=CARTESIAN_POINT ( 'NONE',  ( 15.70011763207405586, 9.048619709455111959, 16.29988236792594591 ) ) ;
#2581=CARTESIAN_POINT ( 'NONE',  ( -15.70011763207405231, -9.048619709455117288, 47.70011763207404698 ) ) ;
#2583=CIRCLE ( 'NONE', #579, 17.50000000000000355 ) ;
#2592=DIRECTION ( 'NONE',  ( 0.000000000000000000, -1.000000000000000000, 0.000000000000000000 ) ) ;
#2594=FACE_OUTER_BOUND ( 'NONE', #3889, .T. ) ;
#2599=VERTEX_POINT ( 'NONE', #573 ) ;
#2600=EDGE_CURVE ( 'NONE', #9251, #9218, #7246, .T. ) ;
#2612=DIRECTION ( 'NONE',  ( 0.000000000000000000, -1.000000000000000000, 0.000000000000000000 ) ) ;
#2614=CARTESIAN_POINT ( 'NONE',  ( 0.000000000000000000, -35.00000000000000000, 32.00000000000000000 ) ) ;
#2616=( BOUNDED_CURVE ( )  B_SPLINE_CURVE ( 3, ( #7588, #3170, #2506, #3795 ),
 .UNSPECIFIED., .F., .F. ) 
 B_SPLINE_CURVE_WITH_KNOTS ( ( 4, 4 ),
 ( 0.000000000000000000, 0.7853981633974485010 ),
 .UNSPECIFIED. ) 
 CURVE ( )  GEOMETRIC_REPRESENTATION_ITEM ( )  RATIONAL_B_SPLINE_CURVE ( ( 1.000000000000000000, 0.9492530216741911220, 0.9492530216741911220, 1.000000000000000000 ) ) 
 REPRESENTATION_ITEM ( '' )  );
#2627=VECTOR ( 'NONE', #2592, 1000.000000000000000 ) ;
#2635=VERTEX_POINT ( 'NONE', #7290 ) ;
#2641=ADVANCED_FACE ( 'NONE', ( #50 ), #9415, .F. ) ;
#2684=DIRECTION ( 'NONE',  ( -0.000000000000000000, -1.000000000000000000, -0.000000000000000000 ) ) ;
#2692=PLANE ( 'NONE',  #6831 ) ;
#2699=ORIENTED_EDGE ( 'NONE', *, *, #9216, .T. ) ;
#2700=DIRECTION ( 'NONE',  ( 0.000000000000000000, -1.000000000000000000, 0.000000000000000000 ) ) ;
#2730=( BOUNDED_CURVE ( )  B_SPLINE_CURVE ( 3, ( #2897, #4291, #3613, #9376 ),
 .UNSPECIFIED., .F., .F. ) 
 B_SPLINE_CURVE_WITH_KNOTS ( ( 4, 4 ),
 ( 2.356194490192344837, 3.141592653589793116 ),
 .UNSPECIFIED. ) 
 CURVE ( )  GEOMETRIC_REPRESENTATION_ITEM ( )  RATIONAL_B_SPLINE_CURVE ( ( 1.000000000000000000, 0.9492530216741911220, 0.9492530216741911220, 1.000000000000000000 ) ) 
 REPRESENTATION_ITEM ( '' )  );
#2731=DIRECTION ( 'NONE',  ( 0.000000000000000000, 1.000000000000000000, 0.000000000000000000 ) ) ;
#2741=EDGE_LOOP ( 'NONE', ( #198, #493, #1242, #3924 ) ) ;
#2750=EDGE_LOOP ( 'NONE', ( #1953, #3829, #8681 ) ) ;
#2753=ORIENTED_EDGE ( 'NONE', *, *, #895, .T. ) ;
#2759=ADVANCED_FACE ( 'NONE', ( #2594 ), #673, .F. ) ;
#2762=EDGE_LOOP ( 'NONE', ( #4778, #5471, #8447, #6329 ) ) ;
#2764=ORIENTED_EDGE ( 'NONE', *, *, #1661, .F. ) ;
#2779=CYLINDRICAL_SURFACE ( 'NONE', #5124, 17.50000000000000000 ) ;
#2788=DIRECTION ( 'NONE',  ( 0.7071067811865460184, 0.000000000000000000, -0.7071067811865489050 ) ) ;
#2800=FACE_OUTER_BOUND ( 'NONE', #2881, .T. ) ;
#2801=ORIENTED_EDGE ( 'NONE', *, *, #4183, .T. ) ;
#2803=ORIENTED_EDGE ( 'NONE', *, *, #3833, .F. ) ;
#2814=ORIENTED_EDGE ( 'NONE', *, *, #7466, .F. ) ;
#2815=DIRECTION ( 'NONE',  ( -1.000000000000000000, 0.000000000000000000, 0.000000000000000000 ) ) ;
#2818=DIRECTION ( 'NONE',  ( 0.000000000000000000, 0.000000000000000000, -1.000000000000000000 ) ) ;
#2821=CARTESIAN_POINT ( 'NONE',  ( -30.99999999999996803, 2.143131898507869037E-15, 49.50000000000000000 ) ) ;
#2825=FACE_OUTER_BOUND ( 'NONE', #1220, .T. ) ;
#2841=EDGE_LOOP ( 'NONE', ( #4779, #4446, #2513, #6225 ) ) ;
#2849=CARTESIAN_POINT ( 'NONE',  ( 27.00000000000000355, -29.99999999999999289, 64.00000000000000000 ) ) ;
#2864=CARTESIAN_POINT ( 'NONE',  ( 32.00000000000000711, 0.000000000000000000, 32.00000000000000000 ) ) ;
#2867=CARTESIAN_POINT ( 'NONE',  ( 27.00000000000000355, 0.000000000000000000, 64.00000000000000000 ) ) ;
#2868=CARTESIAN_POINT ( 'NONE',  ( -12.37436867076458036, -12.37436867076458036, 19.62563132923542142 ) ) ;
#2881=EDGE_LOOP ( 'NONE', ( #2383, #217, #2541, #459 ) ) ;
#2884=VERTEX_POINT ( 'NONE', #4978 ) ;
#2891=CARTESIAN_POINT ( 'NONE',  ( 0.000000000000000000, 0.000000000000000000, 0.000000000000000000 ) ) ;
#2897=CARTESIAN_POINT ( 'NONE',  ( -12.37436867076458036, 12.37436867076458036, 19.62563132923542142 ) ) ;
#2902=CIRCLE ( 'NONE', #9185, 17.50000000000000000 ) ;
#2908=VERTEX_POINT ( 'NONE', #1866 ) ;
#2914=DIRECTION ( 'NONE',  ( -1.000000000000000000, 0.000000000000000000, 0.000000000000000000 ) ) ;
#2931=DIRECTION ( 'NONE',  ( -1.000000000000000000, -0.000000000000000000, -0.000000000000000000 ) ) ;
#2932=DIRECTION ( 'NONE',  ( 0.7071067811865439090, 0.000000000000000000, -0.7071067811865512365 ) ) ;
#2935=ORIENTED_EDGE ( 'NONE', *, *, #192, .T. ) ;
#2936=VERTEX_POINT ( 'NONE', #7094 ) ;
#2937=VECTOR ( 'NONE', #4298, 1000.000000000000114 ) ;
#2942=CYLINDRICAL_SURFACE ( 'NONE', #1515, 17.50000000000000355 ) ;
#2943=ADVANCED_FACE ( 'NONE', ( #5761 ), #2779, .F. ) ;
#2950=AXIS2_PLACEMENT_3D ( 'NONE', #9180, #2700, #7745 ) ;
#2958=CARTESIAN_POINT ( 'NONE',  ( 0.000000000000000000, 0.000000000000000000, 64.00000000000000000 ) ) ;
#2962=ORIENTED_EDGE ( 'NONE', *, *, #6156, .T. ) ;
#2983=CARTESIAN_POINT ( 'NONE',  ( 2.143131898507868248E-15, 17.50000000000000000, 14.49999999999999822 ) ) ;
#2998=EDGE_CURVE ( 'NONE', #2936, #5896, #5863, .T. ) ;
#2999=CARTESIAN_POINT ( 'NONE',  ( -9.048619709455110183, 15.70011763207404876, 16.29988236792595657 ) ) ;
#3006=CARTESIAN_POINT ( 'NONE',  ( -4.703319286132084720, -17.49999999999999645, 14.50000000000000178 ) ) ;
#3008=CARTESIAN_POINT ( 'NONE',  ( -31.99999999999999289, -29.99999999999996447, 0.000000000000000000 ) ) ;
#3009=ORIENTED_EDGE ( 'NONE', *, *, #5368, .T. ) ;
#3011=VECTOR ( 'NONE', #6369, 1000.000000000000000 ) ;
#3013=ORIENTED_EDGE ( 'NONE', *, *, #5966, .F. ) ;
#3016=AXIS2_PLACEMENT_3D ( 'NONE', #213, #4772, #1019 ) ;
#3017=DIRECTION ( 'NONE',  ( 0.000000000000000000, 0.000000000000000000, -1.000000000000000000 ) ) ;
#3022=CIRCLE ( 'NONE', #8552, 17.50000000000000000 ) ;
#3034=CARTESIAN_POINT ( 'NONE',  ( -12.37436867076458036, 12.37436867076458036, 19.62563132923542142 ) ) ;
#3035=CIRCLE ( 'NONE', #5499, 17.50000000000000355 ) ;
#3039=CIRCLE ( 'NONE', #130, 18.50000000000000355 ) ;
#3043=DIRECTION ( 'NONE',  ( -0.000000000000000000, -0.000000000000000000, 1.000000000000000000 ) ) ;
#3049=ORIENTED_EDGE ( 'NONE', *, *, #7347, .T. ) ;
#3057=AXIS2_PLACEMENT_3D ( 'NONE', #3851, #6068, #3998 ) ;
#3060=CARTESIAN_POINT ( 'NONE',  ( 0.000000000000000000, 35.00000000000000000, 32.00000000000000000 ) ) ;
#3064=ORIENTED_EDGE ( 'NONE', *, *, #1007, .T. ) ;
#3069=EDGE_CURVE ( 'NONE', #3097, #8797, #7330, .T. ) ;
#3072=CARTESIAN_POINT ( 'NONE',  ( 0.000000000000000000, -34.99999999999999289, 32.00000000000000000 ) ) ;
#3084=VECTOR ( 'NONE', #4690, 1000.000000000000000 ) ;
#3086=DIRECTION ( 'NONE',  ( 0.000000000000000000, -0.7071067811865451302, -0.7071067811865500152 ) ) ;
#3090=DIRECTION ( 'NONE',  ( 0.000000000000000000, 1.000000000000000000, 0.000000000000000000 ) ) ;
#3093=AXIS2_PLACEMENT_3D ( 'NONE', #7315, #5207, #1654 ) ;
#3095=EDGE_LOOP ( 'NONE', ( #256, #8733, #2962, #7986 ) ) ;
#3097=VERTEX_POINT ( 'NONE', #8679 ) ;
#3103=EDGE_CURVE ( 'NONE', #3697, #794, #7274, .T. ) ;
#3104=CARTESIAN_POINT ( 'NONE',  ( 19.62310601229374285, 19.62310601229374285, 37.12563132923541787 ) ) ;
#3113=ORIENTED_EDGE ( 'NONE', *, *, #5440, .F. ) ;
#3115=EDGE_CURVE ( 'NONE', #3433, #7709, #6574, .T. ) ;
#3116=CARTESIAN_POINT ( 'NONE',  ( 31.00000000000002132, 0.000000000000000000, 14.49999999999999467 ) ) ;
#3126=ADVANCED_FACE ( 'NONE', ( #842 ), #5076, .F. ) ;
#3129=DIRECTION ( 'NONE',  ( -1.000000000000000000, 0.000000000000000000, 0.000000000000000000 ) ) ;
#3130=( NAMED_UNIT ( * ) PLANE_ANGLE_UNIT ( ) SI_UNIT ( $, .RADIAN. ) );
#3141=AXIS2_PLACEMENT_3D ( 'NONE', #791, #4358, #3732 ) ;
#3149=CARTESIAN_POINT ( 'NONE',  ( 2.143131898507868248E-15, -17.50000000000000000, 14.49999999999999822 ) ) ;
#3151=CARTESIAN_POINT ( 'NONE',  ( 2.143131898507868248E-15, 17.50000000000000000, 14.49999999999999822 ) ) ;
#3168=EDGE_LOOP ( 'NONE', ( #4694, #4602, #3113, #9102, #4933, #8928 ) ) ;
#3170=CARTESIAN_POINT ( 'NONE',  ( 17.49999999999999645, -4.703319286132084720, 49.50000000000000000 ) ) ;
#3185=CARTESIAN_POINT ( 'NONE',  ( -30.99999999999996803, 0.000000000000000000, 14.49999999999999467 ) ) ;
#3192=VECTOR ( 'NONE', #6914, 1000.000000000000000 ) ;
#3202=DIRECTION ( 'NONE',  ( -0.7071067811865456854, 3.969829082701935600E-15, -0.7071067811865493491 ) ) ;
#3206=DIRECTION ( 'NONE',  ( -0.7071067811865461294, 0.7071067811865489050, 3.840706726830345682E-15 ) ) ;
#3216=VERTEX_POINT ( 'NONE', #5274 ) ;
#3218=EDGE_CURVE ( 'NONE', #8254, #4201, #4600, .T. ) ;
#3230=EDGE_CURVE ( 'NONE', #7510, #7709, #6858, .T. ) ;
#3246=ADVANCED_FACE ( 'NONE', ( #2800 ), #2122, .F. ) ;
#3253=LINE ( 'NONE', #7182, #1352 ) ;
#3258=EDGE_CURVE ( 'NONE', #7366, #5235, #7165, .T. ) ;
#3271=ORIENTED_EDGE ( 'NONE', *, *, #5604, .T. ) ;
#3280=CARTESIAN_POINT ( 'NONE',  ( -12.37436867076458036, -12.37436867076458036, 44.37436867076458213 ) ) ;
#3288=CARTESIAN_POINT ( 'NONE',  ( -26.99999999999998934, 35.00000000000000000, 64.00000000000000000 ) ) ;
#3289=DIRECTION ( 'NONE',  ( 0.5773502691896290617, -0.5773502691896225114, -0.5773502691896258421 ) ) ;
#3290=LINE ( 'NONE', #8577, #4042 ) ;
#3292=EDGE_CURVE ( 'NONE', #8189, #7366, #4289, .T. ) ;
#3294=CARTESIAN_POINT ( 'NONE',  ( -30.99999999999996803, 0.000000000000000000, 32.00000000000000000 ) ) ;
#3296=EDGE_CURVE ( 'NONE', #2294, #4010, #9471, .T. ) ;
#3309=EDGE_CURVE ( 'NONE', #31, #233, #8700, .T. ) ;
#3315=CARTESIAN_POINT ( 'NONE',  ( 32.00000000000000711, -29.99999999999996447, 64.00000000000000000 ) ) ;
#3326=VECTOR ( 'NONE', #8706, 1000.000000000000000 ) ;
#3335=EDGE_CURVE ( 'NONE', #1694, #3651, #6643, .T. ) ;
#3336=AXIS2_PLACEMENT_3D ( 'NONE', #723, #8699, #1392 ) ;
#3340=CARTESIAN_POINT ( 'NONE',  ( -12.37436867076458036, -12.37436867076458036, 44.37436867076458213 ) ) ;
#3341=EDGE_CURVE ( 'NONE', #4201, #5210, #5643, .T. ) ;
#3345=CARTESIAN_POINT ( 'NONE',  ( 0.000000000000000000, 29.99999999999997158, 64.00000000000000000 ) ) ;
#3346=ORIENTED_EDGE ( 'NONE', *, *, #3341, .F. ) ;
#3350=ORIENTED_EDGE ( 'NONE', *, *, #4314, .F. ) ;
#3352=LINE ( 'NONE', #9247, #2627 ) ;
#3354=CARTESIAN_POINT ( 'NONE',  ( -31.99999999999999289, 2.143131898507868643E-15, 49.50000000000000000 ) ) ;
#3364=PLANE ( 'NONE',  #7872 ) ;
#3377=ORIENTED_EDGE ( 'NONE', *, *, #8257, .T. ) ;
#3392=DIRECTION ( 'NONE',  ( 0.7071067811865460184, 0.000000000000000000, 0.7071067811865489050 ) ) ;
#3393=DIRECTION ( 'NONE',  ( 0.000000000000000000, 0.000000000000000000, -1.000000000000000000 ) ) ;
#3395=LINE ( 'NONE', #4932, #2109 ) ;
#3396=ORIENTED_EDGE ( 'NONE', *, *, #5118, .F. ) ;
#3400=EDGE_CURVE ( 'NONE', #2461, #4035, #642, .T. ) ;
#3404=EDGE_LOOP ( 'NONE', ( #6341, #4047 ) ) ;
#3419=ORIENTED_EDGE ( 'NONE', *, *, #4534, .F. ) ;
#3429=DIRECTION ( 'NONE',  ( 0.000000000000000000, 0.000000000000000000, -1.000000000000000000 ) ) ;
#3433=VERTEX_POINT ( 'NONE', #759 ) ;
#3435=CYLINDRICAL_SURFACE ( 'NONE', #2117, 17.50000000000000355 ) ;
#3436=CARTESIAN_POINT ( 'NONE',  ( 17.50000000000000355, 0.000000000000000000, 49.50000000000000000 ) ) ;
#3442=EDGE_LOOP ( 'NONE', ( #6588, #6847 ) ) ;
#3447=LINE ( 'NONE', #9304, #8814 ) ;
#3452=ADVANCED_FACE ( 'NONE', ( #1474 ), #5722, .F. ) ;
#3456=FACE_BOUND ( 'NONE', #7514, .T. ) ;
#3467=ORIENTED_EDGE ( 'NONE', *, *, #1661, .T. ) ;
#3469=DIRECTION ( 'NONE',  ( 0.000000000000000000, 0.000000000000000000, 1.000000000000000000 ) ) ;
#3474=ORIENTED_EDGE ( 'NONE', *, *, #3103, .F. ) ;
#3484=AXIS2_PLACEMENT_3D ( 'NONE', #5677, #569, #1279 ) ;
#3485=PLANE ( 'NONE',  #8453 ) ;
#3489=CARTESIAN_POINT ( 'NONE',  ( 9.048619709455117288, -15.70011763207404520, 47.70011763207404698 ) ) ;
#3498=DIRECTION ( 'NONE',  ( 0.5773502691896283956, 0.5773502691896228445, 0.5773502691896260641 ) ) ;
#3499=FACE_OUTER_BOUND ( 'NONE', #2750, .T. ) ;
#3504=AXIS2_PLACEMENT_3D ( 'NONE', #2047, #4836, #5028 ) ;
#3505=ORIENTED_EDGE ( 'NONE', *, *, #5830, .F. ) ;
#3519=DIRECTION ( 'NONE',  ( 0.000000000000000000, 0.000000000000000000, 1.000000000000000000 ) ) ;
#3526=LINE ( 'NONE', #3345, #9451 ) ;
#3527=ORIENTED_EDGE ( 'NONE', *, *, #4892, .T. ) ;
#3528=EDGE_CURVE ( 'NONE', #8532, #3216, #8638, .T. ) ;
#3534=EDGE_CURVE ( 'NONE', #2599, #1163, #7197, .T. ) ;
#3541=EDGE_LOOP ( 'NONE', ( #8919, #9014, #267, #8673 ) ) ;
#3556=EDGE_LOOP ( 'NONE', ( #7152, #5024 ) ) ;
#3563=CARTESIAN_POINT ( 'NONE',  ( 27.00000000000000355, 29.99999999999997158, 3.066586833366735950E-16 ) ) ;
#3586=EDGE_CURVE ( 'NONE', #6094, #3807, #1526, .T. ) ;
#3610=CARTESIAN_POINT ( 'NONE',  ( -31.99999999999999289, 0.000000000000000000, 32.00000000000000000 ) ) ;
#3612=ORIENTED_EDGE ( 'NONE', *, *, #1418, .T. ) ;
#3613=CARTESIAN_POINT ( 'NONE',  ( -17.49999999999999645, 4.703319286132086496, 14.49999999999999822 ) ) ;
#3644=CARTESIAN_POINT ( 'NONE',  ( -31.99999999999999289, 29.99999999999997868, 58.99999999999997158 ) ) ;
#3645=VECTOR ( 'NONE', #157, 1000.000000000000114 ) ;
#3651=VERTEX_POINT ( 'NONE', #3116 ) ;
#3665=ORIENTED_EDGE ( 'NONE', *, *, #516, .F. ) ;
#3669=FACE_OUTER_BOUND ( 'NONE', #5252, .T. ) ;
#3676=CARTESIAN_POINT ( 'NONE',  ( 32.00000000000000711, -29.99999999999996447, 5.000000000000031974 ) ) ;
#3697=VERTEX_POINT ( 'NONE', #2456 ) ;
#3726=EDGE_CURVE ( 'NONE', #7789, #8983, #5427, .T. ) ;
#3730=AXIS2_PLACEMENT_3D ( 'NONE', #3315, #8463, #1877 ) ;
#3732=DIRECTION ( 'NONE',  ( 0.000000000000000000, 0.000000000000000000, 1.000000000000000000 ) ) ;
#3735=ORIENTED_EDGE ( 'NONE', *, *, #1838, .T. ) ;
#3752=DIRECTION ( 'NONE',  ( 0.000000000000000000, 0.000000000000000000, -1.000000000000000000 ) ) ;
#3758=EDGE_LOOP ( 'NONE', ( #6968, #1482 ) ) ;
#3761=DIRECTION ( 'NONE',  ( 1.000000000000000000, 0.000000000000000000, 0.000000000000000000 ) ) ;
#3762=CARTESIAN_POINT ( 'NONE',  ( -31.99999999999999289, -34.99999999999999289, 58.99999999999997158 ) ) ;
#3778=EDGE_LOOP ( 'NONE', ( #7425, #7340, #2935, #3346 ) ) ;
#3795=CARTESIAN_POINT ( 'NONE',  ( 12.37436867076458036, -12.37436867076458036, 44.37436867076458213 ) ) ;
#3799=CARTESIAN_POINT ( 'NONE',  ( 31.00000000000002132, 0.000000000000000000, 14.49999999999999467 ) ) ;
#3803=LINE ( 'NONE', #5441, #3890 ) ;
#3807=VERTEX_POINT ( 'NONE', #9067 ) ;
#3811=DIRECTION ( 'NONE',  ( 1.000000000000000000, 0.000000000000000000, 0.000000000000000000 ) ) ;
#3812=CARTESIAN_POINT ( 'NONE',  ( -31.99999999999999289, 0.000000000000000000, 32.00000000000000000 ) ) ;
#3821=FACE_BOUND ( 'NONE', #3442, .T. ) ;
#3829=ORIENTED_EDGE ( 'NONE', *, *, #6438, .T. ) ;
#3830=EDGE_CURVE ( 'NONE', #2599, #7510, #3352, .T. ) ;
#3833=EDGE_CURVE ( 'NONE', #8566, #8795, #6297, .T. ) ;
#3839=UNCERTAINTY_MEASURE_WITH_UNIT (LENGTH_MEASURE( 1.000000000000000082E-05 ), #5393, 'distance_accuracy_value', 'NONE');
#3845=ADVANCED_FACE ( 'NONE', ( #1184 ), #469, .F. ) ;
#3846=CARTESIAN_POINT ( 'NONE',  ( -31.99999999999999289, -29.99999999999996447, 58.99999999999997158 ) ) ;
#3847=ADVANCED_FACE ( 'NONE', ( #5617, #8540 ), #2003, .T. ) ;
#3851=CARTESIAN_POINT ( 'NONE',  ( -31.99999999999999289, 0.000000000000000000, 32.00000000000000000 ) ) ;
#3854=VERTEX_POINT ( 'NONE', #7906 ) ;
#3860=CARTESIAN_POINT ( 'NONE',  ( -12.37436867076458036, 12.37436867076458036, 44.37436867076458213 ) ) ;
#3867=DIRECTION ( 'NONE',  ( -0.7071067811865460184, 0.000000000000000000, -0.7071067811865489050 ) ) ;
#3869=EDGE_CURVE ( 'NONE', #2294, #9473, #4208, .T. ) ;
#3870=MECHANICAL_DESIGN_GEOMETRIC_PRESENTATION_REPRESENTATION('',(#2341),#1195);
#3882=AXIS2_PLACEMENT_3D ( 'NONE', #4059, #1705, #7610 ) ;
#3885=CARTESIAN_POINT ( 'NONE',  ( 0.000000000000000000, 0.000000000000000000, 0.000000000000000000 ) ) ;
#3886=ADVANCED_FACE ( 'NONE', ( #1374 ), #3485, .F. ) ;
#3887=CARTESIAN_POINT ( 'NONE',  ( -9.048619709455111959, -15.70011763207404876, 47.70011763207404698 ) ) ;
#3889=EDGE_LOOP ( 'NONE', ( #6930, #7191, #1329, #1317 ) ) ;
#3890=VECTOR ( 'NONE', #4671, 1000.000000000000000 ) ;
#3894=DIRECTION ( 'NONE',  ( -0.7071067811865490160, -0.7071067811865461294, -0.000000000000000000 ) ) ;
#3909=ORIENTED_EDGE ( 'NONE', *, *, #4070, .T. ) ;
#3915=LINE ( 'NONE', #1849, #6801 ) ;
#3916=DIRECTION ( 'NONE',  ( -0.000000000000000000, -1.000000000000000000, -0.000000000000000000 ) ) ;
#3924=ORIENTED_EDGE ( 'NONE', *, *, #7422, .F. ) ;
#3928=DIRECTION ( 'NONE',  ( -2.775557561562892584E-17, -0.7071067811865493491, 0.7071067811865456854 ) ) ;
#3934=DIRECTION ( 'NONE',  ( 0.7071067811865454633, 0.7071067811865494601, 0.000000000000000000 ) ) ;
#3940=CARTESIAN_POINT ( 'NONE',  ( 2.143131898507868248E-15, -34.00000000000001421, 14.49999999999999822 ) ) ;
#3943=CARTESIAN_POINT ( 'NONE',  ( 0.000000000000000000, 17.50000000000000000, 49.50000000000000000 ) ) ;
#3955=AXIS2_PLACEMENT_3D ( 'NONE', #4575, #7400, #5296 ) ;
#3957=EDGE_CURVE ( 'NONE', #7510, #6770, #7278, .T. ) ;
#3961=CARTESIAN_POINT ( 'NONE',  ( 17.49999999999999645, 4.703319286132082944, 14.49999999999999822 ) ) ;
#3963=SHAPE_REPRESENTATION ( '1-Center Box', ( #1614 ), #4537 ) ;
#3965=VERTEX_POINT ( 'NONE', #2821 ) ;
#3968=EDGE_LOOP ( 'NONE', ( #6439, #1064, #4637 ) ) ;
#3982=VECTOR ( 'NONE', #8536, 1000.000000000000000 ) ;
#3996=DIRECTION ( 'NONE',  ( 1.000000000000000000, -0.000000000000000000, -0.000000000000000000 ) ) ;
#3998=DIRECTION ( 'NONE',  ( 0.000000000000000000, 0.000000000000000000, 1.000000000000000000 ) ) ;
#4006=EDGE_CURVE ( 'NONE', #2635, #9473, #8867, .T. ) ;
#4008=VECTOR ( 'NONE', #5522, 1000.000000000000000 ) ;
#4010=VERTEX_POINT ( 'NONE', #131 ) ;
#4017=CARTESIAN_POINT ( 'NONE',  ( 12.37436867076458036, -12.37436867076458036, 19.62563132923542142 ) ) ;
#4019=DIRECTION ( 'NONE',  ( 1.000000000000000000, 0.000000000000000000, 0.000000000000000000 ) ) ;
#4020=DIRECTION ( 'NONE',  ( 0.000000000000000000, 0.000000000000000000, 1.000000000000000000 ) ) ;
#4035=VERTEX_POINT ( 'NONE', #3151 ) ;
#4042=VECTOR ( 'NONE', #4786, 1000.000000000000114 ) ;
#4043=CARTESIAN_POINT ( 'NONE',  ( -19.62310601229373930, 19.62310601229373930, 37.12563132923542497 ) ) ;
#4047=ORIENTED_EDGE ( 'NONE', *, *, #6576, .T. ) ;
#4048=FACE_OUTER_BOUND ( 'NONE', #3095, .T. ) ;
#4059=CARTESIAN_POINT ( 'NONE',  ( -31.99999999999999289, 0.000000000000000000, 32.00000000000000000 ) ) ;
#4070=EDGE_CURVE ( 'NONE', #3854, #1904, #9062, .T. ) ;
#4073=EDGE_LOOP ( 'NONE', ( #3527, #8777, #4435, #647, #7282, #9375 ) ) ;
#4078=CARTESIAN_POINT ( 'NONE',  ( 0.000000000000000000, -17.50000000000000000, 49.50000000000000000 ) ) ;
#4080=ORIENTED_EDGE ( 'NONE', *, *, #5238, .T. ) ;
#4097=VECTOR ( 'NONE', #6026, 1000.000000000000000 ) ;
#4112=DIRECTION ( 'NONE',  ( 1.000000000000000000, 0.000000000000000000, 0.000000000000000000 ) ) ;
#4115=ORIENTED_EDGE ( 'NONE', *, *, #6949, .T. ) ;
#4117=ORIENTED_EDGE ( 'NONE', *, *, #4439, .F. ) ;
#4132=ADVANCED_FACE ( 'NONE', ( #8440 ), #8291, .T. ) ;
#4143=DIRECTION ( 'NONE',  ( 1.000000000000000000, 0.000000000000000000, 0.000000000000000000 ) ) ;
#4150=( LENGTH_UNIT ( ) NAMED_UNIT ( * ) SI_UNIT ( .MILLI., .METRE. ) );
#4153=CARTESIAN_POINT ( 'NONE',  ( -31.99999999999999289, 35.00000000000000000, 5.000000000000004441 ) ) ;
#4156=PLANE ( 'NONE',  #4207 ) ;
#4157=FACE_OUTER_BOUND ( 'NONE', #2762, .T. ) ;
#4163=EDGE_CURVE ( 'NONE', #5672, #8983, #1544, .T. ) ;
#4171=ORIENTED_EDGE ( 'NONE', *, *, #8162, .F. ) ;
#4173=CONICAL_SURFACE ( 'NONE', #39, 18.50000000000001776, 0.7853981633974431720 ) ;
#4175=CARTESIAN_POINT ( 'NONE',  ( 27.00000000000000355, 35.00000000000000000, 5.000000000000004441 ) ) ;
#4176=CARTESIAN_POINT ( 'NONE',  ( 12.37436867076458036, 12.37436867076458036, 19.62563132923542142 ) ) ;
#4183=EDGE_CURVE ( 'NONE', #3097, #4382, #359, .T. ) ;
#4184=PLANE ( 'NONE',  #2950 ) ;
#4192=SHAPE_REPRESENTATION_RELATIONSHIP ( 'NONE' , 'NONE' ,  #3963, #5431 ) ;
#4194=CARTESIAN_POINT ( 'NONE',  ( 27.00000000000000355, -34.99999999999999289, 5.000000000000004441 ) ) ;
#4196=LINE ( 'NONE', #4153, #8545 ) ;
#4199=DIRECTION ( 'NONE',  ( 0.000000000000000000, 0.000000000000000000, 1.000000000000000000 ) ) ;
#4201=VERTEX_POINT ( 'NONE', #7042 ) ;
#4206=LINE ( 'NONE', #8584, #8539 ) ;
#4207=AXIS2_PLACEMENT_3D ( 'NONE', #7716, #3289, #274 ) ;
#4208=LINE ( 'NONE', #4930, #5997 ) ;
#4231=CARTESIAN_POINT ( 'NONE',  ( 32.00000000000000711, 29.99999999999997868, 58.99999999999997158 ) ) ;
#4236=VECTOR ( 'NONE', #3519, 1000.000000000000000 ) ;
#4237=PLANE ( 'NONE',  #5632 ) ;
#4239=EDGE_CURVE ( 'NONE', #794, #3697, #2321, .T. ) ;
#4240=ORIENTED_EDGE ( 'NONE', *, *, #4239, .F. ) ;
#4261=EDGE_CURVE ( 'NONE', #9251, #4913, #2529, .T. ) ;
#4265=VECTOR ( 'NONE', #7732, 1000.000000000000000 ) ;
#4266=AXIS2_PLACEMENT_3D ( 'NONE', #1058, #9119, #5480 ) ;
#4277=CARTESIAN_POINT ( 'NONE',  ( 17.50000000000000355, 0.000000000000000000, 14.49999999999999822 ) ) ;
#4278=DIRECTION ( 'NONE',  ( -0.5773502691896290617, -0.5773502691896258421, 0.5773502691896225114 ) ) ;
#4279=ORIENTED_EDGE ( 'NONE', *, *, #3292, .F. ) ;
#4281=ORIENTED_EDGE ( 'NONE', *, *, #104, .T. ) ;
#4282=CIRCLE ( 'NONE', #1297, 18.50000000000001776 ) ;
#4289=LINE ( 'NONE', #3563, #6714 ) ;
#4290=VERTEX_POINT ( 'NONE', #4741 ) ;
#4291=CARTESIAN_POINT ( 'NONE',  ( -15.70011763207404876, 9.048619709455115512, 16.29988236792595302 ) ) ;
#4293=DIRECTION ( 'NONE',  ( -1.000000000000000000, 0.000000000000000000, 0.000000000000000000 ) ) ;
#4298=DIRECTION ( 'NONE',  ( 0.000000000000000000, 0.7071067811865493491, -0.7071067811865456854 ) ) ;
#4311=CARTESIAN_POINT ( 'NONE',  ( -26.99999999999998934, 35.00000000000000000, 5.000000000000004441 ) ) ;
#4314=EDGE_CURVE ( 'NONE', #7012, #9473, #8615, .T. ) ;
#4322=FACE_OUTER_BOUND ( 'NONE', #3968, .T. ) ;
#4334=AXIS2_PLACEMENT_3D ( 'NONE', #443, #4143, #9220 ) ;
#4344=CARTESIAN_POINT ( 'NONE',  ( 32.00000000000000711, 0.000000000000000000, 13.49999999999999822 ) ) ;
#4358=DIRECTION ( 'NONE',  ( -0.000000000000000000, 1.000000000000000000, -0.000000000000000000 ) ) ;
#4359=CARTESIAN_POINT ( 'NONE',  ( 0.000000000000000000, 0.000000000000000000, 0.000000000000000000 ) ) ;
#4361=ORIENTED_EDGE ( 'NONE', *, *, #9287, .F. ) ;
#4362=AXIS2_PLACEMENT_3D ( 'NONE', #3072, #91, #3017 ) ;
#4370=ORIENTED_EDGE ( 'NONE', *, *, #6377, .T. ) ;
#4382=VERTEX_POINT ( 'NONE', #7173 ) ;
#4385=LINE ( 'NONE', #4441, #4097 ) ;
#4387=CYLINDRICAL_SURFACE ( 'NONE', #9378, 17.50000000000000355 ) ;
#4407=DIRECTION ( 'NONE',  ( 0.000000000000000000, 0.000000000000000000, -1.000000000000000000 ) ) ;
#4408=CARTESIAN_POINT ( 'NONE',  ( 15.70011763207405231, 9.048619709455117288, 47.70011763207404698 ) ) ;
#4415=CONICAL_SURFACE ( 'NONE', #8559, 17.50000000000000000, 0.7853981633974552734 ) ;
#4428=CARTESIAN_POINT ( 'NONE',  ( 0.000000000000000000, 0.000000000000000000, 63.00000000000002842 ) ) ;
#4435=ORIENTED_EDGE ( 'NONE', *, *, #5536, .F. ) ;
#4439=EDGE_CURVE ( 'NONE', #7709, #1163, #2174, .T. ) ;
#4441=CARTESIAN_POINT ( 'NONE',  ( 0.000000000000000000, -35.00000000000000000, 49.50000000000000000 ) ) ;
#4443=DIRECTION ( 'NONE',  ( -0.000000000000000000, -0.000000000000000000, 1.000000000000000000 ) ) ;
#4446=ORIENTED_EDGE ( 'NONE', *, *, #4439, .T. ) ;
#4448=ORIENTED_EDGE ( 'NONE', *, *, #3830, .T. ) ;
#4466=VERTEX_POINT ( 'NONE', #5206 ) ;
#4471=PRODUCT ( '1-Center Box', '1-Center Box', '', ( #5236 ) ) ;
#4472=FACE_OUTER_BOUND ( 'NONE', #2841, .T. ) ;
#4475=EDGE_CURVE ( 'NONE', #7912, #6850, #7508, .T. ) ;
#4481=DIRECTION ( 'NONE',  ( -1.000000000000000000, 0.000000000000000000, 0.000000000000000000 ) ) ;
#4489=ORIENTED_EDGE ( 'NONE', *, *, #1007, .F. ) ;
#4516=CARTESIAN_POINT ( 'NONE',  ( 0.000000000000000000, 0.000000000000000000, 64.00000000000000000 ) ) ;
#4530=ADVANCED_FACE ( 'NONE', ( #7409 ), #2942, .F. ) ;
#4531=CARTESIAN_POINT ( 'NONE',  ( -12.37436867076458036, 12.37436867076458036, 44.37436867076458213 ) ) ;
#4534=EDGE_CURVE ( 'NONE', #8189, #2635, #2276, .T. ) ;
#4535=EDGE_CURVE ( 'NONE', #1699, #6770, #822, .T. ) ;
#4537=( GEOMETRIC_REPRESENTATION_CONTEXT ( 3 ) GLOBAL_UNCERTAINTY_ASSIGNED_CONTEXT ( ( #1627 ) ) GLOBAL_UNIT_ASSIGNED_CONTEXT ( ( #4150, #7077, #1212 ) ) REPRESENTATION_CONTEXT ( 'NONE', 'WORKASPACE' ) );
#4538=ORIENTED_EDGE ( 'NONE', *, *, #6688, .T. ) ;
#4539=DIRECTION ( 'NONE',  ( 1.000000000000000000, 0.000000000000000000, 0.000000000000000000 ) ) ;
#4544=DIRECTION ( 'NONE',  ( 0.000000000000000000, -1.000000000000000000, 0.000000000000000000 ) ) ;
#4547=FACE_BOUND ( 'NONE', #3556, .T. ) ;
#4548=EDGE_CURVE ( 'NONE', #794, #3854, #5980, .T. ) ;
#4549=DIRECTION ( 'NONE',  ( 8.659560562354963673E-17, -0.7071067811865451302, 0.7071067811865500152 ) ) ;
#4575=CARTESIAN_POINT ( 'NONE',  ( 0.000000000000000000, 0.000000000000000000, 64.00000000000000000 ) ) ;
#4578=ORIENTED_EDGE ( 'NONE', *, *, #3830, .F. ) ;
#4579=CARTESIAN_POINT ( 'NONE',  ( -18.49999999999997513, 2.265596578422600241E-15, 64.00000000000000000 ) ) ;
#4582=FACE_OUTER_BOUND ( 'NONE', #1001, .T. ) ;
#4585=DIRECTION ( 'NONE',  ( 0.000000000000000000, 0.000000000000000000, -1.000000000000000000 ) ) ;
#4600=LINE ( 'NONE', #1209, #8855 ) ;
#4602=ORIENTED_EDGE ( 'NONE', *, *, #6377, .F. ) ;
#4604=CARTESIAN_POINT ( 'NONE',  ( 27.00000000000000355, 35.00000000000000000, 59.00000000000000000 ) ) ;
#4618=CARTESIAN_POINT ( 'NONE',  ( -31.99999999999999289, -34.99999999999999289, 5.000000000000004441 ) ) ;
#4621=CARTESIAN_POINT ( 'NONE',  ( -26.99999999999996092, -29.99999999999996447, 0.000000000000000000 ) ) ;
#4630=ADVANCED_FACE ( 'NONE', ( #8991, #7749 ), #1069, .F. ) ;
#4631=( BOUNDED_CURVE ( )  B_SPLINE_CURVE ( 3, ( #8185, #8142, #1601, #4531 ),
 .UNSPECIFIED., .F., .T. ) 
 B_SPLINE_CURVE_WITH_KNOTS ( ( 4, 4 ),
 ( 0.000000000000000000, 0.7853981633974485010 ),
 .UNSPECIFIED. ) 
 CURVE ( )  GEOMETRIC_REPRESENTATION_ITEM ( )  RATIONAL_B_SPLINE_CURVE ( ( 1.000000000000000000, 0.9492530216741911220, 0.9492530216741911220, 1.000000000000000000 ) ) 
 REPRESENTATION_ITEM ( '' )  );
#4637=ORIENTED_EDGE ( 'NONE', *, *, #3586, .F. ) ;
#4640=DIRECTION ( 'NONE',  ( -0.7071067811865463515, 8.659560562354919300E-17, 0.7071067811865487940 ) ) ;
#4649=CARTESIAN_POINT ( 'NONE',  ( -17.50000000000000355, 2.143131898507868643E-15, 1.000000000000021760 ) ) ;
#4663=EDGE_CURVE ( 'NONE', #1694, #2461, #5981, .T. ) ;
#4664=CIRCLE ( 'NONE', #5583, 18.49999999999998934 ) ;
#4670=ADVANCED_FACE ( 'NONE', ( #6936 ), #6079, .T. ) ;
#4671=DIRECTION ( 'NONE',  ( -0.000000000000000000, 1.000000000000000000, -0.000000000000000000 ) ) ;
#4672=EDGE_LOOP ( 'NONE', ( #668, #4117, #8487, #4578 ) ) ;
#4675=ORIENTED_EDGE ( 'NONE', *, *, #758, .T. ) ;
#4681=AXIS2_PLACEMENT_3D ( 'NONE', #2192, #7423, #5940 ) ;
#4690=DIRECTION ( 'NONE',  ( 0.000000000000000000, 0.000000000000000000, 1.000000000000000000 ) ) ;
#4694=ORIENTED_EDGE ( 'NONE', *, *, #1731, .F. ) ;
#4696=ADVANCED_FACE ( 'NONE', ( #5358 ), #1885, .F. ) ;
#4700=DIRECTION ( 'NONE',  ( 0.000000000000000000, 0.000000000000000000, 1.000000000000000000 ) ) ;
#4705=PLANE ( 'NONE',  #884 ) ;
#4726=FACE_OUTER_BOUND ( 'NONE', #7608, .T. ) ;
#4737=CYLINDRICAL_SURFACE ( 'NONE', #3882, 17.50000000000000355 ) ;
#4740=AXIS2_PLACEMENT_3D ( 'NONE', #7275, #8906, #176 ) ;
#4741=CARTESIAN_POINT ( 'NONE',  ( 12.37436867076458036, -12.37436867076458036, 44.37436867076458213 ) ) ;
#4744=ORIENTED_EDGE ( 'NONE', *, *, #6826, .T. ) ;
#4756=CARTESIAN_POINT ( 'NONE',  ( -12.37436867076458036, -12.37436867076458036, 44.37436867076458213 ) ) ;
#4763=LINE ( 'NONE', #7642, #9120 ) ;
#4765=DIRECTION ( 'NONE',  ( -0.000000000000000000, 1.000000000000000000, -0.000000000000000000 ) ) ;
#4771=DIRECTION ( 'NONE',  ( 0.7071067811865493491, 0.000000000000000000, -0.7071067811865456854 ) ) ;
#4772=DIRECTION ( 'NONE',  ( 0.7071067811865494601, 0.000000000000000000, -0.7071067811865455743 ) ) ;
#4778=ORIENTED_EDGE ( 'NONE', *, *, #6947, .F. ) ;
#4779=ORIENTED_EDGE ( 'NONE', *, *, #3115, .T. ) ;
#4786=DIRECTION ( 'NONE',  ( 0.000000000000000000, 0.7071067811865456854, 0.7071067811865493491 ) ) ;
#4788=ORIENTED_EDGE ( 'NONE', *, *, #6421, .F. ) ;
#4791=DIRECTION ( 'NONE',  ( 0.000000000000000000, 0.000000000000000000, -1.000000000000000000 ) ) ;
#4803=EDGE_CURVE ( 'NONE', #3965, #6009, #9268, .T. ) ;
#4807=ORIENTED_EDGE ( 'NONE', *, *, #7230, .F. ) ;
#4820=ORIENTED_EDGE ( 'NONE', *, *, #7995, .F. ) ;
#4836=DIRECTION ( 'NONE',  ( -0.000000000000000000, -0.000000000000000000, 1.000000000000000000 ) ) ;
#4837=CARTESIAN_POINT ( 'NONE',  ( -31.99999999999999289, 0.000000000000000000, 32.00000000000000000 ) ) ;
#4847=EDGE_LOOP ( 'NONE', ( #2065, #6986, #9354, #3419 ) ) ;
#4862=EDGE_CURVE ( 'NONE', #233, #31, #7203, .T. ) ;
#4867=AXIS2_PLACEMENT_3D ( 'NONE', #7339, #1432, #761 ) ;
#4879=( BOUNDED_CURVE ( )  B_SPLINE_CURVE ( 3, ( #9035, #4043, #6886, #436 ),
 .UNSPECIFIED., .F., .F. ) 
 B_SPLINE_CURVE_WITH_KNOTS ( ( 4, 4 ),
 ( 5.497787143782137953, 7.068583470577034511 ),
 .UNSPECIFIED. ) 
 CURVE ( )  GEOMETRIC_REPRESENTATION_ITEM ( )  RATIONAL_B_SPLINE_CURVE ( ( 1.000000000000000000, 0.8047378541243649375, 0.8047378541243649375, 1.000000000000000000 ) ) 
 REPRESENTATION_ITEM ( '' )  );
#4892=EDGE_CURVE ( 'NONE', #8532, #3965, #6764, .T. ) ;
#4913=VERTEX_POINT ( 'NONE', #6639 ) ;
#4915=CARTESIAN_POINT ( 'NONE',  ( 0.000000000000000000, -34.00000000000001421, 49.50000000000000000 ) ) ;
#4917=AXIS2_PLACEMENT_3D ( 'NONE', #3060, #4544, #81 ) ;
#4918=DIRECTION ( 'NONE',  ( 0.7071067811865456854, 0.7071067811865493491, 3.960316634274392569E-15 ) ) ;
#4924=EDGE_LOOP ( 'NONE', ( #5011, #4240, #8567, #3665 ) ) ;
#4930=CARTESIAN_POINT ( 'NONE',  ( 32.00000000000000711, -29.99999999999996447, 64.00000000000000000 ) ) ;
#4932=CARTESIAN_POINT ( 'NONE',  ( -31.99999999999999289, 2.143131898507868643E-15, 49.50000000000000000 ) ) ;
#4933=ORIENTED_EDGE ( 'NONE', *, *, #3335, .T. ) ;
#4948=ORIENTED_EDGE ( 'NONE', *, *, #5760, .F. ) ;
#4950=LINE ( 'NONE', #2024, #7242 ) ;
#4964=CARTESIAN_POINT ( 'NONE',  ( -15.70011763207405586, -9.048619709455111959, 16.29988236792594591 ) ) ;
#4967=DIRECTION ( 'NONE',  ( -0.000000000000000000, -0.000000000000000000, -1.000000000000000000 ) ) ;
#4974=FACE_OUTER_BOUND ( 'NONE', #8338, .T. ) ;
#4978=CARTESIAN_POINT ( 'NONE',  ( 0.000000000000000000, 17.50000000000000000, 49.50000000000000000 ) ) ;
#4980=ORIENTED_EDGE ( 'NONE', *, *, #4006, .T. ) ;
#5005=DIRECTION ( 'NONE',  ( 1.000000000000000000, -0.000000000000000000, 0.000000000000000000 ) ) ;
#5007=VECTOR ( 'NONE', #2287, 1000.000000000000000 ) ;
#5011=ORIENTED_EDGE ( 'NONE', *, *, #5238, .F. ) ;
#5018=LINE ( 'NONE', #644, #2937 ) ;
#5020=CARTESIAN_POINT ( 'NONE',  ( 0.000000000000000000, 0.000000000000000000, 1.000000000000021760 ) ) ;
#5024=ORIENTED_EDGE ( 'NONE', *, *, #4862, .T. ) ;
#5028=DIRECTION ( 'NONE',  ( 1.000000000000000000, 0.000000000000000000, 0.000000000000000000 ) ) ;
#5033=CIRCLE ( 'NONE', #218, 18.50000000000001776 ) ;
#5059=CARTESIAN_POINT ( 'NONE',  ( -31.99999999999999289, 0.000000000000000000, 32.00000000000000000 ) ) ;
#5063=ADVANCED_FACE ( 'NONE', ( #1010 ), #8312, .F. ) ;
#5076=CYLINDRICAL_SURFACE ( 'NONE', #3141, 17.50000000000000000 ) ;
#5104=EDGE_CURVE ( 'NONE', #8532, #4913, #4763, .T. ) ;
#5109=CIRCLE ( 'NONE', #8496, 17.50000000000000355 ) ;
#5116=ADVANCED_FACE ( 'NONE', ( #8415 ), #1827, .T. ) ;
#5118=EDGE_CURVE ( 'NONE', #2884, #4466, #388, .T. ) ;
#5124=AXIS2_PLACEMENT_3D ( 'NONE', #7007, #5712, #1914 ) ;
#5125=ORIENTED_EDGE ( 'NONE', *, *, #6511, .T. ) ;
#5132=ADVANCED_FACE ( 'NONE', ( #6164 ), #2692, .T. ) ;
#5165=CLOSED_SHELL ( 'NONE', ( #5829, #2759, #2641, #6444, #1253, #8513, #6632, #1100, #2943, #3452, #6417, #660, #4530, #4630, #7418, #6135, #6710, #5420, #3847, #6070, #3126, #4696, #6935, #5840, #4132, #4670, #6921, #7284, #78, #9109, #5063, #5132, #5116, #1931, #7820, #2495, #5592, #7243, #8524, #3886, #2432, #1417, #1703, #3246, #2128, #60, #8247, #3845, #5916, #7533 ) ) ;
#5176=DIRECTION ( 'NONE',  ( 0.000000000000000000, -1.000000000000000000, 0.000000000000000000 ) ) ;
#5177=CARTESIAN_POINT ( 'NONE',  ( 12.37436867076458036, 12.37436867076458036, 44.37436867076458213 ) ) ;
#5179=CIRCLE ( 'NONE', #1038, 18.50000000000000355 ) ;
#5197=DIRECTION ( 'NONE',  ( 1.000000000000000000, -0.000000000000000000, -0.000000000000000000 ) ) ;
#5204=PLANE ( 'NONE',  #1574 ) ;
#5206=CARTESIAN_POINT ( 'NONE',  ( 12.37436867076458036, 12.37436867076458036, 44.37436867076458213 ) ) ;
#5207=DIRECTION ( 'NONE',  ( 1.000000000000000000, 0.000000000000000000, 0.000000000000000000 ) ) ;
#5210=VERTEX_POINT ( 'NONE', #6619 ) ;
#5215=CARTESIAN_POINT ( 'NONE',  ( 2.143131898507868248E-15, 17.50000000000000000, 14.49999999999999822 ) ) ;
#5235=VERTEX_POINT ( 'NONE', #4175 ) ;
#5236=PRODUCT_CONTEXT ( 'NONE', #1981, 'mechanical' ) ;
#5238=EDGE_CURVE ( 'NONE', #3697, #1904, #3447, .T. ) ;
#5252=EDGE_LOOP ( 'NONE', ( #219, #5644, #6592, #2407 ) ) ;
#5274=CARTESIAN_POINT ( 'NONE',  ( -31.99999999999999289, 2.265596578422605368E-15, 13.49999999999998401 ) ) ;
#5280=CONICAL_SURFACE ( 'NONE', #8188, 17.50000000000000355, 0.7853981633974466137 ) ;
#5296=DIRECTION ( 'NONE',  ( -1.000000000000000000, 0.000000000000000000, 0.000000000000000000 ) ) ;
#5316=CARTESIAN_POINT ( 'NONE',  ( 17.50000000000000355, 0.000000000000000000, 0.000000000000000000 ) ) ;
#5329=CARTESIAN_POINT ( 'NONE',  ( 0.000000000000000000, 0.000000000000000000, 0.000000000000000000 ) ) ;
#5345=CARTESIAN_POINT ( 'NONE',  ( -31.99999999999999289, -29.99999999999996447, 5.000000000000005329 ) ) ;
#5346=VECTOR ( 'NONE', #8206, 1000.000000000000114 ) ;
#5354=VECTOR ( 'NONE', #1370, 1000.000000000000114 ) ;
#5358=FACE_OUTER_BOUND ( 'NONE', #9240, .T. ) ;
#5363=EDGE_LOOP ( 'NONE', ( #9045, #9071, #2494, #6183 ) ) ;
#5367=LINE ( 'NONE', #221, #140 ) ;
#5368=EDGE_CURVE ( 'NONE', #2936, #1890, #6232, .T. ) ;
#5374=DIRECTION ( 'NONE',  ( 0.000000000000000000, 0.000000000000000000, -1.000000000000000000 ) ) ;
#5377=ORIENTED_EDGE ( 'NONE', *, *, #2249, .T. ) ;
#5382=CARTESIAN_POINT ( 'NONE',  ( 0.000000000000000000, -29.99999999999999289, 64.00000000000000000 ) ) ;
#5390=CARTESIAN_POINT ( 'NONE',  ( 31.00000000000002132, 2.143131898507869037E-15, 49.50000000000000000 ) ) ;
#5393=( LENGTH_UNIT ( ) NAMED_UNIT ( * ) SI_UNIT ( .MILLI., .METRE. ) );
#5399=CARTESIAN_POINT ( 'NONE',  ( 27.00000000000000355, -34.99999999999999289, 64.00000000000000000 ) ) ;
#5400=PLANE ( 'NONE',  #3016 ) ;
#5409=DIRECTION ( 'NONE',  ( 0.5773502691896285066, 0.5773502691896228445, -0.5773502691896261751 ) ) ;
#5411=CARTESIAN_POINT ( 'NONE',  ( 0.000000000000000000, 34.00000000000001421, 32.00000000000000000 ) ) ;
#5420=ADVANCED_FACE ( 'NONE', ( #4547, #6091 ), #2390, .F. ) ;
#5427=LINE ( 'NONE', #6245, #8707 ) ;
#5431=ADVANCED_BREP_SHAPE_REPRESENTATION ( '', ( #6309, #1614 ), #4537 ) ;
#5439=DIRECTION ( 'NONE',  ( -0.000000000000000000, -1.000000000000000000, -0.000000000000000000 ) ) ;
#5440=EDGE_CURVE ( 'NONE', #2461, #4466, #2302, .T. ) ;
#5441=CARTESIAN_POINT ( 'NONE',  ( 2.143131898507868248E-15, -35.00000000000000000, 14.49999999999999822 ) ) ;
#5457=FACE_OUTER_BOUND ( 'NONE', #1263, .T. ) ;
#5460=DIRECTION ( 'NONE',  ( -0.000000000000000000, -0.000000000000000000, 1.000000000000000000 ) ) ;
#5461=DIRECTION ( 'NONE',  ( 1.000000000000000000, 0.000000000000000000, 0.000000000000000000 ) ) ;
#5470=LINE ( 'NONE', #1863, #8104 ) ;
#5471=ORIENTED_EDGE ( 'NONE', *, *, #8930, .F. ) ;
#5480=DIRECTION ( 'NONE',  ( -1.000000000000000000, 0.000000000000000000, 0.000000000000000000 ) ) ;
#5482=AXIS2_PLACEMENT_3D ( 'NONE', #1696, #6216, #7507 ) ;
#5485=( NAMED_UNIT ( * ) SI_UNIT ( $, .STERADIAN. ) SOLID_ANGLE_UNIT ( ) );
#5486=LINE ( 'NONE', #8417, #1332 ) ;
#5498=DIRECTION ( 'NONE',  ( 0.000000000000000000, 0.000000000000000000, 1.000000000000000000 ) ) ;
#5499=AXIS2_PLACEMENT_3D ( 'NONE', #5579, #5530, #7737 ) ;
#5504=DIRECTION ( 'NONE',  ( 0.000000000000000000, 0.000000000000000000, 1.000000000000000000 ) ) ;
#5512=CARTESIAN_POINT ( 'NONE',  ( -17.49999999999999645, -4.703319286132083832, 49.50000000000000000 ) ) ;
#5522=DIRECTION ( 'NONE',  ( 0.7071067811865439090, 8.659560562354889717E-17, -0.7071067811865512365 ) ) ;
#5529=VECTOR ( 'NONE', #8514, 999.9999999999998863 ) ;
#5530=DIRECTION ( 'NONE',  ( -0.000000000000000000, -0.000000000000000000, -1.000000000000000000 ) ) ;
#5533=CARTESIAN_POINT ( 'NONE',  ( 0.000000000000000000, -34.00000000000001421, 32.00000000000000000 ) ) ;
#5536=EDGE_CURVE ( 'NONE', #5896, #6890, #7880, .T. ) ;
#5545=DIRECTION ( 'NONE',  ( -0.000000000000000000, 1.000000000000000000, -0.000000000000000000 ) ) ;
#5557=EDGE_CURVE ( 'NONE', #3651, #7789, #6215, .T. ) ;
#5562=ORIENTED_EDGE ( 'NONE', *, *, #474, .F. ) ;
#5566=ORIENTED_EDGE ( 'NONE', *, *, #8162, .T. ) ;
#5568=LINE ( 'NONE', #6815, #2441 ) ;
#5578=AXIS2_PLACEMENT_3D ( 'NONE', #9001, #5409, #3867 ) ;
#5579=CARTESIAN_POINT ( 'NONE',  ( 0.000000000000000000, 0.000000000000000000, 1.000000000000021760 ) ) ;
#5580=DIRECTION ( 'NONE',  ( 0.000000000000000000, -1.000000000000000000, 0.000000000000000000 ) ) ;
#5583=AXIS2_PLACEMENT_3D ( 'NONE', #9145, #5608, #1995 ) ;
#5589=AXIS2_PLACEMENT_3D ( 'NONE', #752, #6667, #5941 ) ;
#5592=ADVANCED_FACE ( 'NONE', ( #7808 ), #4156, .T. ) ;
#5596=EDGE_LOOP ( 'NONE', ( #6759, #1823, #8740, #1085 ) ) ;
#5597=ORIENTED_EDGE ( 'NONE', *, *, #7911, .T. ) ;
#5602=VECTOR ( 'NONE', #1421, 1000.000000000000000 ) ;
#5604=EDGE_CURVE ( 'NONE', #4382, #1163, #9237, .T. ) ;
#5608=DIRECTION ( 'NONE',  ( 0.000000000000000000, 1.000000000000000000, 0.000000000000000000 ) ) ;
#5617=FACE_BOUND ( 'NONE', #479, .T. ) ;
#5620=DIRECTION ( 'NONE',  ( 1.000000000000000000, -0.000000000000000000, -0.000000000000000000 ) ) ;
#5626=CARTESIAN_POINT ( 'NONE',  ( 27.00000000000000355, 35.00000000000000000, 59.00000000000000000 ) ) ;
#5632=AXIS2_PLACEMENT_3D ( 'NONE', #7168, #590, #1355 ) ;
#5643=CIRCLE ( 'NONE', #414, 18.49999999999998934 ) ;
#5644=ORIENTED_EDGE ( 'NONE', *, *, #2137, .F. ) ;
#5672=VERTEX_POINT ( 'NONE', #4344 ) ;
#5677=CARTESIAN_POINT ( 'NONE',  ( 0.000000000000000000, -35.00000000000000000, 32.00000000000000000 ) ) ;
#5699=CARTESIAN_POINT ( 'NONE',  ( 27.00000000000000355, -34.99999999999999289, 5.000000000000003553 ) ) ;
#5701=CARTESIAN_POINT ( 'NONE',  ( -26.99999999999998934, -34.99999999999999289, 64.00000000000000000 ) ) ;
#5712=DIRECTION ( 'NONE',  ( -0.000000000000000000, 1.000000000000000000, -0.000000000000000000 ) ) ;
#5714=EDGE_CURVE ( 'NONE', #7012, #2635, #5018, .T. ) ;
#5722=CYLINDRICAL_SURFACE ( 'NONE', #3484, 17.50000000000000000 ) ;
#5737=DIRECTION ( 'NONE',  ( -0.000000000000000000, 1.000000000000000000, 0.000000000000000000 ) ) ;
#5741=DIRECTION ( 'NONE',  ( 0.000000000000000000, 0.000000000000000000, 1.000000000000000000 ) ) ;
#5759=DIRECTION ( 'NONE',  ( 0.000000000000000000, 1.000000000000000000, 0.000000000000000000 ) ) ;
#5760=EDGE_CURVE ( 'NONE', #6515, #2884, #6854, .T. ) ;
#5761=FACE_OUTER_BOUND ( 'NONE', #8285, .T. ) ;
#5777=VECTOR ( 'NONE', #8835, 1000.000000000000114 ) ;
#5781=CARTESIAN_POINT ( 'NONE',  ( 0.000000000000000000, -29.99999999999999289, 64.00000000000000000 ) ) ;
#5782=ORIENTED_EDGE ( 'NONE', *, *, #8369, .T. ) ;
#5793=ORIENTED_EDGE ( 'NONE', *, *, #5440, .T. ) ;
#5798=DIRECTION ( 'NONE',  ( -1.000000000000000000, 0.000000000000000000, 0.000000000000000000 ) ) ;
#5815=ORIENTED_EDGE ( 'NONE', *, *, #8365, .T. ) ;
#5817=EDGE_LOOP ( 'NONE', ( #4171, #1746, #8317, #6376 ) ) ;
#5823=CYLINDRICAL_SURFACE ( 'NONE', #7049, 17.50000000000000355 ) ;
#5826=ORIENTED_EDGE ( 'NONE', *, *, #6627, .F. ) ;
#5829=ADVANCED_FACE ( 'NONE', ( #826 ), #8468, .F. ) ;
#5830=EDGE_CURVE ( 'NONE', #6890, #6515, #4631, .T. ) ;
#5833=CARTESIAN_POINT ( 'NONE',  ( 0.000000000000000000, 0.000000000000000000, 63.00000000000002842 ) ) ;
#5839=ORIENTED_EDGE ( 'NONE', *, *, #6006, .T. ) ;
#5840=ADVANCED_FACE ( 'NONE', ( #8281 ), #4387, .F. ) ;
#5863=( BOUNDED_CURVE ( )  B_SPLINE_CURVE ( 3, ( #2868, #8007, #7279, #2292 ),
 .UNSPECIFIED., .F., .T. ) 
 B_SPLINE_CURVE_WITH_KNOTS ( ( 4, 4 ),
 ( 2.356194490192345281, 3.926990816987240951 ),
 .UNSPECIFIED. ) 
 CURVE ( )  GEOMETRIC_REPRESENTATION_ITEM ( )  RATIONAL_B_SPLINE_CURVE ( ( 1.000000000000000000, 0.8047378541243652705, 0.8047378541243652705, 1.000000000000000000 ) ) 
 REPRESENTATION_ITEM ( '' )  );
#5864=ORIENTED_EDGE ( 'NONE', *, *, #2137, .T. ) ;
#5867=CARTESIAN_POINT ( 'NONE',  ( 32.00000000000000711, 29.99999999999997158, 0.000000000000000000 ) ) ;
#5872=CARTESIAN_POINT ( 'NONE',  ( 0.000000000000000000, -34.99999999999999289, 32.00000000000000000 ) ) ;
#5875=ORIENTED_EDGE ( 'NONE', *, *, #6627, .T. ) ;
#5876=DIRECTION ( 'NONE',  ( 0.000000000000000000, 0.000000000000000000, -1.000000000000000000 ) ) ;
#5889=CARTESIAN_POINT ( 'NONE',  ( -26.99999999999998934, 32.49999999999998579, 61.50000000000000000 ) ) ;
#5892=DIRECTION ( 'NONE',  ( 0.7071067811865456854, 0.000000000000000000, 0.7071067811865493491 ) ) ;
#5896=VERTEX_POINT ( 'NONE', #3280 ) ;
#5905=DIRECTION ( 'NONE',  ( -0.7071067811865439090, 0.000000000000000000, -0.7071067811865512365 ) ) ;
#5915=CARTESIAN_POINT ( 'NONE',  ( -31.99999999999999289, 0.000000000000000000, 32.00000000000000000 ) ) ;
#5916=ADVANCED_FACE ( 'NONE', ( #6894 ), #4173, .F. ) ;
#5931=ORIENTED_EDGE ( 'NONE', *, *, #608, .F. ) ;
#5935=CARTESIAN_POINT ( 'NONE',  ( -12.37436867076458036, 12.37436867076458036, 19.62563132923542142 ) ) ;
#5937=CIRCLE ( 'NONE', #8393, 17.50000000000000355 ) ;
#5940=DIRECTION ( 'NONE',  ( 0.000000000000000000, 0.000000000000000000, -1.000000000000000000 ) ) ;
#5941=DIRECTION ( 'NONE',  ( -0.7071067811865494601, 0.000000000000000000, 0.7071067811865454633 ) ) ;
#5966=EDGE_CURVE ( 'NONE', #7881, #3433, #1886, .T. ) ;
#5980=LINE ( 'NONE', #2377, #6132 ) ;
#5981=( BOUNDED_CURVE ( )  B_SPLINE_CURVE ( 3, ( #6217, #3961, #2567, #9042 ),
 .UNSPECIFIED., .F., .T. ) 
 B_SPLINE_CURVE_WITH_KNOTS ( ( 4, 4 ),
 ( 3.141592653589793116, 3.926990816987241395 ),
 .UNSPECIFIED. ) 
 CURVE ( )  GEOMETRIC_REPRESENTATION_ITEM ( )  RATIONAL_B_SPLINE_CURVE ( ( 1.000000000000000000, 0.9492530216741911220, 0.9492530216741911220, 1.000000000000000000 ) ) 
 REPRESENTATION_ITEM ( '' )  );
#5985=EDGE_LOOP ( 'NONE', ( #5377, #8423, #1470, #3009, #4115, #6563, #4820 ) ) ;
#5993=CARTESIAN_POINT ( 'NONE',  ( 12.37436867076458036, 12.37436867076458036, 44.37436867076458213 ) ) ;
#5997=VECTOR ( 'NONE', #6384, 1000.000000000000000 ) ;
#6003=AXIS2_PLACEMENT_3D ( 'NONE', #5411, #8483, #8333 ) ;
#6006=EDGE_CURVE ( 'NONE', #2331, #8797, #6937, .T. ) ;
#6009=VERTEX_POINT ( 'NONE', #7843 ) ;
#6015=CARTESIAN_POINT ( 'NONE',  ( -30.99999999999996803, 0.000000000000000000, 32.00000000000000000 ) ) ;
#6017=LINE ( 'NONE', #3799, #7390 ) ;
#6022=ORIENTED_EDGE ( 'NONE', *, *, #8947, .T. ) ;
#6026=DIRECTION ( 'NONE',  ( -0.000000000000000000, 1.000000000000000000, -0.000000000000000000 ) ) ;
#6029=CARTESIAN_POINT ( 'NONE',  ( 27.00000000000000355, -34.99999999999999289, 0.000000000000000000 ) ) ;
#6068=DIRECTION ( 'NONE',  ( -1.000000000000000000, -0.000000000000000000, -0.000000000000000000 ) ) ;
#6070=ADVANCED_FACE ( 'NONE', ( #7983 ), #1934, .F. ) ;
#6074=CARTESIAN_POINT ( 'NONE',  ( 0.000000000000000000, -34.99999999999999289, 13.50000000000001243 ) ) ;
#6075=ORIENTED_EDGE ( 'NONE', *, *, #7667, .F. ) ;
#6079=PLANE ( 'NONE',  #1203 ) ;
#6091=FACE_OUTER_BOUND ( 'NONE', #6799, .T. ) ;
#6094=VERTEX_POINT ( 'NONE', #4231 ) ;
#6097=EDGE_LOOP ( 'NONE', ( #8179, #8596, #8380 ) ) ;
#6100=DIRECTION ( 'NONE',  ( 1.000000000000000000, 0.000000000000000000, 0.000000000000000000 ) ) ;
#6106=DIRECTION ( 'NONE',  ( -0.000000000000000000, -0.000000000000000000, -1.000000000000000000 ) ) ;
#6107=CARTESIAN_POINT ( 'NONE',  ( 27.00000000000000355, 35.00000000000000000, 59.00000000000000000 ) ) ;
#6109=ORIENTED_EDGE ( 'NONE', *, *, #4239, .T. ) ;
#6132=VECTOR ( 'NONE', #8897, 1000.000000000000000 ) ;
#6135=ADVANCED_FACE ( 'NONE', ( #6685, #4472 ), #6598, .F. ) ;
#6153=CARTESIAN_POINT ( 'NONE',  ( 0.000000000000000000, -35.00000000000000000, 49.50000000000000000 ) ) ;
#6156=EDGE_CURVE ( 'NONE', #3651, #5672, #6017, .T. ) ;
#6164=FACE_OUTER_BOUND ( 'NONE', #4847, .T. ) ;
#6179=VECTOR ( 'NONE', #5737, 1000.000000000000000 ) ;
#6183=ORIENTED_EDGE ( 'NONE', *, *, #4183, .F. ) ;
#6200=VECTOR ( 'NONE', #1812, 1000.000000000000114 ) ;
#6210=ORIENTED_EDGE ( 'NONE', *, *, #9052, .F. ) ;
#6215=CIRCLE ( 'NONE', #7118, 17.50000000000000000 ) ;
#6216=DIRECTION ( 'NONE',  ( 0.000000000000000000, 0.000000000000000000, 1.000000000000000000 ) ) ;
#6217=CARTESIAN_POINT ( 'NONE',  ( 17.50000000000000355, 0.000000000000000000, 14.49999999999999822 ) ) ;
#6225=ORIENTED_EDGE ( 'NONE', *, *, #5966, .T. ) ;
#6230=CARTESIAN_POINT ( 'NONE',  ( 32.00000000000000711, 0.000000000000000000, 32.00000000000000000 ) ) ;
#6232=( BOUNDED_CURVE ( )  B_SPLINE_CURVE ( 3, ( #2443, #1566, #3006, #8246 ),
 .UNSPECIFIED., .F., .T. ) 
 B_SPLINE_CURVE_WITH_KNOTS ( ( 4, 4 ),
 ( 2.356194490192344837, 3.141592653589793116 ),
 .UNSPECIFIED. ) 
 CURVE ( )  GEOMETRIC_REPRESENTATION_ITEM ( )  RATIONAL_B_SPLINE_CURVE ( ( 1.000000000000000000, 0.9492530216741911220, 0.9492530216741911220, 1.000000000000000000 ) ) 
 REPRESENTATION_ITEM ( '' )  );
#6237=( BOUNDED_CURVE ( )  B_SPLINE_CURVE ( 3, ( #9250, #3489, #9352, #4078 ),
 .UNSPECIFIED., .F., .F. ) 
 B_SPLINE_CURVE_WITH_KNOTS ( ( 4, 4 ),
 ( 5.497787143782137953, 6.283185307179586232 ),
 .UNSPECIFIED. ) 
 CURVE ( )  GEOMETRIC_REPRESENTATION_ITEM ( )  RATIONAL_B_SPLINE_CURVE ( ( 1.000000000000000000, 0.9492530216741911220, 0.9492530216741911220, 1.000000000000000000 ) ) 
 REPRESENTATION_ITEM ( '' )  );
#6245=CARTESIAN_POINT ( 'NONE',  ( 31.00000000000002132, 2.143131898507868643E-15, 49.50000000000000000 ) ) ;
#6252=VECTOR ( 'NONE', #3206, 1000.000000000000114 ) ;
#6265=VECTOR ( 'NONE', #3086, 1000.000000000000114 ) ;
#6268=CIRCLE ( 'NONE', #3336, 18.50000000000001776 ) ;
#6297=LINE ( 'NONE', #9201, #4008 ) ;
#6307=CARTESIAN_POINT ( 'NONE',  ( 15.70011763207404876, -9.048619709455115512, 16.29988236792595302 ) ) ;
#6309=MANIFOLD_SOLID_BREP ( 'Pah2', #5165 ) ;
#6313=ORIENTED_EDGE ( 'NONE', *, *, #3258, .F. ) ;
#6315=CARTESIAN_POINT ( 'NONE',  ( -26.99999999999996092, 29.99999999999997158, 0.000000000000000000 ) ) ;
#6317=CARTESIAN_POINT ( 'NONE',  ( -31.99999999999999289, -34.99999999999999289, 5.000000000000004441 ) ) ;
#6329=ORIENTED_EDGE ( 'NONE', *, *, #4862, .F. ) ;
#6333=CARTESIAN_POINT ( 'NONE',  ( -26.99999999999997513, -32.49999999999997868, 2.500000000000002220 ) ) ;
#6341=ORIENTED_EDGE ( 'NONE', *, *, #4163, .T. ) ;
#6346=CARTESIAN_POINT ( 'NONE',  ( 17.49999999999999645, -4.703319286132086496, 14.49999999999999822 ) ) ;
#6369=DIRECTION ( 'NONE',  ( 0.7071067811865463515, 0.000000000000000000, 0.7071067811865487940 ) ) ;
#6374=DIRECTION ( 'NONE',  ( -0.7071067811865461294, -0.7071067811865489050, -3.776607970617559778E-15 ) ) ;
#6376=ORIENTED_EDGE ( 'NONE', *, *, #192, .F. ) ;
#6377=EDGE_CURVE ( 'NONE', #4466, #7912, #8917, .T. ) ;
#6384=DIRECTION ( 'NONE',  ( 0.000000000000000000, 0.000000000000000000, -1.000000000000000000 ) ) ;
#6388=EDGE_LOOP ( 'NONE', ( #3049, #7616, #5864, #5782 ) ) ;
#6398=ORIENTED_EDGE ( 'NONE', *, *, #895, .F. ) ;
#6417=ADVANCED_FACE ( 'NONE', ( #2197 ), #7381, .F. ) ;
#6421=EDGE_CURVE ( 'NONE', #2884, #794, #1045, .T. ) ;
#6422=EDGE_CURVE ( 'NONE', #1673, #3807, #5470, .T. ) ;
#6423=LINE ( 'NONE', #5701, #1127 ) ;
#6430=VECTOR ( 'NONE', #2142, 1000.000000000000114 ) ;
#6432=AXIS2_PLACEMENT_3D ( 'NONE', #6015, #2931, #2164 ) ;
#6438=EDGE_CURVE ( 'NONE', #7709, #6770, #5568, .T. ) ;
#6439=ORIENTED_EDGE ( 'NONE', *, *, #9287, .T. ) ;
#6444=ADVANCED_FACE ( 'NONE', ( #8395 ), #4415, .F. ) ;
#6448=PLANE ( 'NONE',  #9008 ) ;
#6467=VECTOR ( 'NONE', #9440, 1000.000000000000114 ) ;
#6482=CARTESIAN_POINT ( 'NONE',  ( 2.265596578422603791E-15, 35.00000000000000000, 13.49999999999999822 ) ) ;
#6488=ORIENTED_EDGE ( 'NONE', *, *, #3400, .F. ) ;
#6511=EDGE_CURVE ( 'NONE', #7510, #4010, #9152, .T. ) ;
#6515=VERTEX_POINT ( 'NONE', #7577 ) ;
#6521=CARTESIAN_POINT ( 'NONE',  ( -26.99999999999998934, -34.99999999999999289, 58.99999999999997158 ) ) ;
#6552=AXIS2_PLACEMENT_3D ( 'NONE', #271, #454, #3469 ) ;
#6563=ORIENTED_EDGE ( 'NONE', *, *, #2522, .T. ) ;
#6570=CARTESIAN_POINT ( 'NONE',  ( -26.99999999999998934, -34.99999999999999289, 58.99999999999997158 ) ) ;
#6574=LINE ( 'NONE', #8819, #5602 ) ;
#6576=EDGE_CURVE ( 'NONE', #8983, #5672, #3039, .T. ) ;
#6588=ORIENTED_EDGE ( 'NONE', *, *, #2191, .T. ) ;
#6592=ORIENTED_EDGE ( 'NONE', *, *, #6438, .F. ) ;
#6596=LINE ( 'NONE', #5867, #9470 ) ;
#6598=PLANE ( 'NONE',  #2025 ) ;
#6606=CARTESIAN_POINT ( 'NONE',  ( -26.99999999999998934, -34.99999999999999289, 64.00000000000000000 ) ) ;
#6610=ORIENTED_EDGE ( 'NONE', *, *, #2522, .F. ) ;
#6616=AXIS2_PLACEMENT_3D ( 'NONE', #7092, #8729, #8627 ) ;
#6619=CARTESIAN_POINT ( 'NONE',  ( 0.000000000000000000, -34.99999999999999289, 13.50000000000001243 ) ) ;
#6627=EDGE_CURVE ( 'NONE', #7881, #8797, #9392, .T. ) ;
#6632=ADVANCED_FACE ( 'NONE', ( #4974 ), #3435, .F. ) ;
#6633=ORIENTED_EDGE ( 'NONE', *, *, #4475, .F. ) ;
#6639=CARTESIAN_POINT ( 'NONE',  ( -17.50000000000000355, 2.143131898507868643E-15, 14.49999999999999822 ) ) ;
#6643=LINE ( 'NONE', #6687, #873 ) ;
#6650=CARTESIAN_POINT ( 'NONE',  ( 0.000000000000000000, 0.000000000000000000, 0.000000000000000000 ) ) ;
#6659=ORIENTED_EDGE ( 'NONE', *, *, #1294, .F. ) ;
#6662=LINE ( 'NONE', #5316, #5007 ) ;
#6667=DIRECTION ( 'NONE',  ( -0.5773502691896258421, -0.5773502691896225114, -0.5773502691896290617 ) ) ;
#6674=EDGE_LOOP ( 'NONE', ( #8137, #1721, #1390, #967, #8822, #4744, #4281 ) ) ;
#6685=FACE_BOUND ( 'NONE', #3758, .T. ) ;
#6687=CARTESIAN_POINT ( 'NONE',  ( -31.99999999999999289, 0.000000000000000000, 14.49999999999999467 ) ) ;
#6688=EDGE_CURVE ( 'NONE', #2599, #4382, #2001, .T. ) ;
#6690=LINE ( 'NONE', #6074, #6265 ) ;
#6703=CARTESIAN_POINT ( 'NONE',  ( -31.99999999999999289, 35.00000000000000000, 59.00000000000000000 ) ) ;
#6710=ADVANCED_FACE ( 'NONE', ( #3821, #6763 ), #8811, .F. ) ;
#6714=VECTOR ( 'NONE', #9422, 1000.000000000000114 ) ;
#6734=ORIENTED_EDGE ( 'NONE', *, *, #1551, .F. ) ;
#6755=DIRECTION ( 'NONE',  ( 1.000000000000000000, -0.000000000000000000, -0.000000000000000000 ) ) ;
#6759=ORIENTED_EDGE ( 'NONE', *, *, #4892, .F. ) ;
#6760=CARTESIAN_POINT ( 'NONE',  ( 0.000000000000000000, 0.000000000000000000, 0.000000000000000000 ) ) ;
#6763=FACE_OUTER_BOUND ( 'NONE', #6388, .T. ) ;
#6764=CIRCLE ( 'NONE', #6432, 17.50000000000000355 ) ;
#6770=VERTEX_POINT ( 'NONE', #6570 ) ;
#6789=EDGE_LOOP ( 'NONE', ( #7430, #5562, #4361, #7777 ) ) ;
#6796=DIRECTION ( 'NONE',  ( -0.7071067811865501263, 0.000000000000000000, 0.7071067811865450192 ) ) ;
#6798=ORIENTED_EDGE ( 'NONE', *, *, #2322, .T. ) ;
#6799=EDGE_LOOP ( 'NONE', ( #4448, #5125, #9162, #2139 ) ) ;
#6801=VECTOR ( 'NONE', #4640, 1000.000000000000000 ) ;
#6813=ORIENTED_EDGE ( 'NONE', *, *, #7230, .T. ) ;
#6815=CARTESIAN_POINT ( 'NONE',  ( -26.99999999999998934, -34.99999999999999289, 58.99999999999997158 ) ) ;
#6826=EDGE_CURVE ( 'NONE', #4035, #1161, #1687, .T. ) ;
#6831=AXIS2_PLACEMENT_3D ( 'NONE', #8593, #9360, #5580 ) ;
#6841=DIRECTION ( 'NONE',  ( -0.7071067811865455743, 0.000000000000000000, -0.7071067811865494601 ) ) ;
#6847=ORIENTED_EDGE ( 'NONE', *, *, #3341, .T. ) ;
#6850=VERTEX_POINT ( 'NONE', #1797 ) ;
#6854=( BOUNDED_CURVE ( )  B_SPLINE_CURVE ( 3, ( #3860, #1505, #1553, #7455 ),
 .UNSPECIFIED., .F., .F. ) 
 B_SPLINE_CURVE_WITH_KNOTS ( ( 4, 4 ),
 ( 5.497787143782137953, 6.283185307179586232 ),
 .UNSPECIFIED. ) 
 CURVE ( )  GEOMETRIC_REPRESENTATION_ITEM ( )  RATIONAL_B_SPLINE_CURVE ( ( 1.000000000000000000, 0.9492530216741911220, 0.9492530216741911220, 1.000000000000000000 ) ) 
 REPRESENTATION_ITEM ( '' )  );
#6858=LINE ( 'NONE', #9009, #9305 ) ;
#6862=CARTESIAN_POINT ( 'NONE',  ( -18.50000000000001776, 0.000000000000000000, 0.000000000000000000 ) ) ;
#6865=CONICAL_SURFACE ( 'NONE', #6552, 17.50000000000000000, 0.7853981633974552734 ) ;
#6866=CARTESIAN_POINT ( 'NONE',  ( -26.99999999999998934, 35.00000000000000000, 5.000000000000004441 ) ) ;
#6883=CARTESIAN_POINT ( 'NONE',  ( 4.703319286132083832, 17.49999999999999645, 49.50000000000000000 ) ) ;
#6886=CARTESIAN_POINT ( 'NONE',  ( -19.62310601229374285, 19.62310601229374285, 26.87436867076458569 ) ) ;
#6890=VERTEX_POINT ( 'NONE', #270 ) ;
#6894=FACE_OUTER_BOUND ( 'NONE', #1221, .T. ) ;
#6896=EDGE_CURVE ( 'NONE', #4010, #3807, #1750, .T. ) ;
#6897=VECTOR ( 'NONE', #8141, 1000.000000000000000 ) ;
#6903=DIRECTION ( 'NONE',  ( -0.000000000000000000, -0.000000000000000000, 1.000000000000000000 ) ) ;
#6904=PLANE ( 'NONE',  #5578 ) ;
#6914=DIRECTION ( 'NONE',  ( -0.000000000000000000, 1.000000000000000000, -0.000000000000000000 ) ) ;
#6921=ADVANCED_FACE ( 'NONE', ( #8957 ), #6904, .T. ) ;
#6922=AXIS2_PLACEMENT_3D ( 'NONE', #6230, #402, #272 ) ;
#6925=DIRECTION ( 'NONE',  ( -0.000000000000000000, -0.7071067811865455743, -0.7071067811865494601 ) ) ;
#6928=CARTESIAN_POINT ( 'NONE',  ( -17.50000000000000355, 2.143131898507868643E-15, 63.00000000000002842 ) ) ;
#6930=ORIENTED_EDGE ( 'NONE', *, *, #2249, .F. ) ;
#6935=ADVANCED_FACE ( 'NONE', ( #5457 ), #4737, .F. ) ;
#6936=FACE_OUTER_BOUND ( 'NONE', #7634, .T. ) ;
#6937=LINE ( 'NONE', #7703, #6179 ) ;
#6947=EDGE_CURVE ( 'NONE', #1286, #233, #3915, .T. ) ;
#6949=EDGE_CURVE ( 'NONE', #1890, #2562, #9217, .T. ) ;
#6954=EDGE_LOOP ( 'NONE', ( #186, #265, #5931, #7686 ) ) ;
#6966=CARTESIAN_POINT ( 'NONE',  ( 27.00000000000000355, -34.99999999999999289, 58.99999999999997158 ) ) ;
#6968=ORIENTED_EDGE ( 'NONE', *, *, #1095, .T. ) ;
#6983=FACE_OUTER_BOUND ( 'NONE', #4672, .T. ) ;
#6986=ORIENTED_EDGE ( 'NONE', *, *, #7911, .F. ) ;
#6989=CARTESIAN_POINT ( 'NONE',  ( 9.048619709455110183, -15.70011763207404876, 16.29988236792595657 ) ) ;
#7007=CARTESIAN_POINT ( 'NONE',  ( 0.000000000000000000, -35.00000000000000000, 32.00000000000000000 ) ) ;
#7012=VERTEX_POINT ( 'NONE', #4194 ) ;
#7013=CONICAL_SURFACE ( 'NONE', #9458, 18.50000000000001776, 0.7853981633974412846 ) ;
#7018=DIRECTION ( 'NONE',  ( 0.7071067811865454633, -0.7071067811865494601, 0.000000000000000000 ) ) ;
#7027=FACE_OUTER_BOUND ( 'NONE', #184, .T. ) ;
#7042=CARTESIAN_POINT ( 'NONE',  ( 2.265596578422601819E-15, -34.99999999999999289, 50.49999999999998579 ) ) ;
#7047=ORIENTED_EDGE ( 'NONE', *, *, #3335, .F. ) ;
#7049=AXIS2_PLACEMENT_3D ( 'NONE', #5915, #5197, #1494 ) ;
#7054=PLANE ( 'NONE',  #705 ) ;
#7055=CARTESIAN_POINT ( 'NONE',  ( 0.000000000000000000, -34.99999999999999289, 32.00000000000000000 ) ) ;
#7077=( NAMED_UNIT ( * ) PLANE_ANGLE_UNIT ( ) SI_UNIT ( $, .RADIAN. ) );
#7092=CARTESIAN_POINT ( 'NONE',  ( 0.000000000000000000, 0.000000000000000000, 0.000000000000000000 ) ) ;
#7094=CARTESIAN_POINT ( 'NONE',  ( -12.37436867076458036, -12.37436867076458036, 19.62563132923542142 ) ) ;
#7108=CARTESIAN_POINT ( 'NONE',  ( -26.99999999999998934, -29.99999999999999289, 64.00000000000000000 ) ) ;
#7118=AXIS2_PLACEMENT_3D ( 'NONE', #9143, #5461, #4020 ) ;
#7126=AXIS2_PLACEMENT_3D ( 'NONE', #8360, #3894, #2412 ) ;
#7129=ORIENTED_EDGE ( 'NONE', *, *, #6688, .F. ) ;
#7152=ORIENTED_EDGE ( 'NONE', *, *, #3309, .T. ) ;
#7158=CARTESIAN_POINT ( 'NONE',  ( -31.99999999999999289, -29.99999999999996447, 5.000000000000004441 ) ) ;
#7165=LINE ( 'NONE', #7259, #7930 ) ;
#7168=CARTESIAN_POINT ( 'NONE',  ( -31.99999999999999289, 29.99999999999997868, 64.00000000000000000 ) ) ;
#7171=CARTESIAN_POINT ( 'NONE',  ( 17.50000000000000355, 0.000000000000000000, 63.00000000000002842 ) ) ;
#7173=CARTESIAN_POINT ( 'NONE',  ( -26.99999999999998934, 35.00000000000000000, 59.00000000000000000 ) ) ;
#7177=DIRECTION ( 'NONE',  ( -1.000000000000000000, 0.000000000000000000, 0.000000000000000000 ) ) ;
#7182=CARTESIAN_POINT ( 'NONE',  ( 27.00000000000000355, 29.99999999999997158, -3.066586833366757151E-16 ) ) ;
#7189=CONICAL_SURFACE ( 'NONE', #3057, 18.50000000000001776, 0.7853981633974412846 ) ;
#7191=ORIENTED_EDGE ( 'NONE', *, *, #3833, .T. ) ;
#7197=LINE ( 'NONE', #3644, #8093 ) ;
#7203=CIRCLE ( 'NONE', #9350, 18.49999999999997513 ) ;
#7230=EDGE_CURVE ( 'NONE', #4290, #2562, #1371, .T. ) ;
#7237=ORIENTED_EDGE ( 'NONE', *, *, #1218, .T. ) ;
#7242=VECTOR ( 'NONE', #2612, 1000.000000000000000 ) ;
#7243=ADVANCED_FACE ( 'NONE', ( #3669 ), #5204, .F. ) ;
#7246=LINE ( 'NONE', #1626, #7568 ) ;
#7258=CARTESIAN_POINT ( 'NONE',  ( -31.99999999999999289, 29.99999999999997868, 58.99999999999997158 ) ) ;
#7259=CARTESIAN_POINT ( 'NONE',  ( 29.50000000000000711, 32.49999999999999289, 5.000000000000018652 ) ) ;
#7266=AXIS2_PLACEMENT_3D ( 'NONE', #3885, #6106, #7682 ) ;
#7270=ORIENTED_EDGE ( 'NONE', *, *, #2413, .F. ) ;
#7274=CIRCLE ( 'NONE', #4681, 17.50000000000000000 ) ;
#7275=CARTESIAN_POINT ( 'NONE',  ( -31.99999999999999289, -34.99999999999999289, 64.00000000000000000 ) ) ;
#7278=LINE ( 'NONE', #6521, #6467 ) ;
#7279=CARTESIAN_POINT ( 'NONE',  ( -19.62310601229373930, -19.62310601229373930, 37.12563132923541076 ) ) ;
#7282=ORIENTED_EDGE ( 'NONE', *, *, #8299, .F. ) ;
#7284=ADVANCED_FACE ( 'NONE', ( #4582 ), #7452, .T. ) ;
#7288=DIRECTION ( 'NONE',  ( -0.7071067811865525687, 8.659560562354873694E-17, -0.7071067811865425767 ) ) ;
#7290=CARTESIAN_POINT ( 'NONE',  ( 27.00000000000000355, -29.99999999999996447, 0.000000000000000000 ) ) ;
#7299=DIRECTION ( 'NONE',  ( 0.000000000000000000, 0.000000000000000000, 1.000000000000000000 ) ) ;
#7303=CARTESIAN_POINT ( 'NONE',  ( -31.99999999999999289, -34.99999999999999289, 64.00000000000000000 ) ) ;
#7313=CARTESIAN_POINT ( 'NONE',  ( -31.99999999999999289, -34.99999999999999289, 58.99999999999997158 ) ) ;
#7315=CARTESIAN_POINT ( 'NONE',  ( 31.00000000000002132, 0.000000000000000000, 32.00000000000000000 ) ) ;
#7317=ORIENTED_EDGE ( 'NONE', *, *, #5368, .F. ) ;
#7324=AXIS2_PLACEMENT_3D ( 'NONE', #4428, #7299, #8887 ) ;
#7330=LINE ( 'NONE', #4311, #8810 ) ;
#7331=PLANE ( 'NONE',  #5589 ) ;
#7339=CARTESIAN_POINT ( 'NONE',  ( -31.99999999999999289, 0.000000000000000000, 32.00000000000000000 ) ) ;
#7340=ORIENTED_EDGE ( 'NONE', *, *, #1218, .F. ) ;
#7347=EDGE_CURVE ( 'NONE', #7012, #1699, #9040, .T. ) ;
#7360=CARTESIAN_POINT ( 'NONE',  ( 12.37436867076458036, -12.37436867076458036, 44.37436867076458213 ) ) ;
#7366=VERTEX_POINT ( 'NONE', #2514 ) ;
#7372=AXIS2_PLACEMENT_3D ( 'NONE', #9236, #1167, #4019 ) ;
#7381=CYLINDRICAL_SURFACE ( 'NONE', #7950, 17.50000000000000355 ) ;
#7385=CARTESIAN_POINT ( 'NONE',  ( 29.50000000000000711, 29.99999999999997513, 61.49999999999998579 ) ) ;
#7390=VECTOR ( 'NONE', #2932, 1000.000000000000000 ) ;
#7400=DIRECTION ( 'NONE',  ( 0.000000000000000000, 0.000000000000000000, -1.000000000000000000 ) ) ;
#7409=FACE_OUTER_BOUND ( 'NONE', #9104, .T. ) ;
#7418=ADVANCED_FACE ( 'NONE', ( #3456, #7027 ), #4184, .F. ) ;
#7422=EDGE_CURVE ( 'NONE', #6094, #2294, #4950, .T. ) ;
#7423=DIRECTION ( 'NONE',  ( 0.000000000000000000, 1.000000000000000000, 0.000000000000000000 ) ) ;
#7425=ORIENTED_EDGE ( 'NONE', *, *, #3218, .F. ) ;
#7430=ORIENTED_EDGE ( 'NONE', *, *, #3258, .T. ) ;
#7452=PLANE ( 'NONE',  #7713 ) ;
#7455=CARTESIAN_POINT ( 'NONE',  ( 0.000000000000000000, 17.50000000000000000, 49.50000000000000000 ) ) ;
#7458=ORIENTED_EDGE ( 'NONE', *, *, #2998, .T. ) ;
#7461=EDGE_LOOP ( 'NONE', ( #977, #8419, #872, #7677 ) ) ;
#7462=ORIENTED_EDGE ( 'NONE', *, *, #6949, .F. ) ;
#7466=EDGE_CURVE ( 'NONE', #3433, #2331, #7698, .T. ) ;
#7480=DIRECTION ( 'NONE',  ( -0.000000000000000000, -0.000000000000000000, 1.000000000000000000 ) ) ;
#7488=ORIENTED_EDGE ( 'NONE', *, *, #8326, .T. ) ;
#7507=DIRECTION ( 'NONE',  ( 1.000000000000000000, 0.000000000000000000, 0.000000000000000000 ) ) ;
#7508=LINE ( 'NONE', #8228, #8119 ) ;
#7510=VERTEX_POINT ( 'NONE', #7108 ) ;
#7514=EDGE_LOOP ( 'NONE', ( #3909, #120 ) ) ;
#7526=EDGE_LOOP ( 'NONE', ( #502, #6398, #7129, #8956 ) ) ;
#7533=ADVANCED_FACE ( 'NONE', ( #4048 ), #798, .F. ) ;
#7568=VECTOR ( 'NONE', #5905, 1000.000000000000000 ) ;
#7577=CARTESIAN_POINT ( 'NONE',  ( -12.37436867076458036, 12.37436867076458036, 44.37436867076458213 ) ) ;
#7588=CARTESIAN_POINT ( 'NONE',  ( 17.50000000000000355, 0.000000000000000000, 49.50000000000000000 ) ) ;
#7608=EDGE_LOOP ( 'NONE', ( #412, #1936, #885, #9206 ) ) ;
#7610=DIRECTION ( 'NONE',  ( 0.000000000000000000, 0.000000000000000000, -1.000000000000000000 ) ) ;
#7616=ORIENTED_EDGE ( 'NONE', *, *, #4535, .T. ) ;
#7634=EDGE_LOOP ( 'NONE', ( #2129, #293, #5826 ) ) ;
#7640=PLANE ( 'NONE',  #4266 ) ;
#7642=CARTESIAN_POINT ( 'NONE',  ( -31.99999999999999289, 0.000000000000000000, 14.49999999999999467 ) ) ;
#7667=EDGE_CURVE ( 'NONE', #1699, #2294, #8745, .T. ) ;
#7677=ORIENTED_EDGE ( 'NONE', *, *, #8369, .F. ) ;
#7682=DIRECTION ( 'NONE',  ( -1.000000000000000000, 0.000000000000000000, 0.000000000000000000 ) ) ;
#7686=ORIENTED_EDGE ( 'NONE', *, *, #8947, .F. ) ;
#7691=CARTESIAN_POINT ( 'NONE',  ( 9.048619709455111959, 15.70011763207404876, 47.70011763207404698 ) ) ;
#7698=LINE ( 'NONE', #7158, #2345 ) ;
#7703=CARTESIAN_POINT ( 'NONE',  ( -26.99999999999996092, 35.00000000000000000, 0.000000000000000000 ) ) ;
#7709=VERTEX_POINT ( 'NONE', #3846 ) ;
#7712=CARTESIAN_POINT ( 'NONE',  ( 4.703319286132082055, -17.49999999999999645, 14.50000000000000178 ) ) ;
#7713=AXIS2_PLACEMENT_3D ( 'NONE', #8318, #6841, #8989 ) ;
#7716=CARTESIAN_POINT ( 'NONE',  ( 27.00000000000000355, -34.99999999999999289, 5.000000000000004441 ) ) ;
#7732=DIRECTION ( 'NONE',  ( 1.000000000000000000, -0.000000000000000000, -0.000000000000000000 ) ) ;
#7737=DIRECTION ( 'NONE',  ( -1.000000000000000000, 0.000000000000000000, 0.000000000000000000 ) ) ;
#7745=DIRECTION ( 'NONE',  ( 0.000000000000000000, -0.000000000000000000, -1.000000000000000000 ) ) ;
#7749=FACE_OUTER_BOUND ( 'NONE', #8955, .T. ) ;
#7750=CARTESIAN_POINT ( 'NONE',  ( 0.000000000000000000, 0.000000000000000000, 0.000000000000000000 ) ) ;
#7762=PRODUCT_DEFINITION ( 'UNKNOWN', '', #8067, #2307 ) ;
#7777=ORIENTED_EDGE ( 'NONE', *, *, #8326, .F. ) ;
#7789=VERTEX_POINT ( 'NONE', #5390 ) ;
#7796=DIRECTION ( 'NONE',  ( 1.000000000000000000, 0.000000000000000000, 0.000000000000000000 ) ) ;
#7802=ORIENTED_EDGE ( 'NONE', *, *, #9052, .T. ) ;
#7808=FACE_OUTER_BOUND ( 'NONE', #1386, .T. ) ;
#7817=DIRECTION ( 'NONE',  ( 1.000000000000000000, -0.000000000000000000, -0.000000000000000000 ) ) ;
#7820=ADVANCED_FACE ( 'NONE', ( #1137 ), #7054, .T. ) ;
#7843=CARTESIAN_POINT ( 'NONE',  ( -31.99999999999999289, 0.000000000000000000, 50.50000000000001421 ) ) ;
#7872=AXIS2_PLACEMENT_3D ( 'NONE', #5626, #3498, #2788 ) ;
#7880=( BOUNDED_CURVE ( )  B_SPLINE_CURVE ( 3, ( #3340, #2581, #5512, #405 ),
 .UNSPECIFIED., .F., .F. ) 
 B_SPLINE_CURVE_WITH_KNOTS ( ( 4, 4 ),
 ( 5.497787143782137953, 6.283185307179586232 ),
 .UNSPECIFIED. ) 
 CURVE ( )  GEOMETRIC_REPRESENTATION_ITEM ( )  RATIONAL_B_SPLINE_CURVE ( ( 1.000000000000000000, 0.9492530216741911220, 0.9492530216741911220, 1.000000000000000000 ) ) 
 REPRESENTATION_ITEM ( '' )  );
#7881=VERTEX_POINT ( 'NONE', #7905 ) ;
#7899=VERTEX_POINT ( 'NONE', #8003 ) ;
#7905=CARTESIAN_POINT ( 'NONE',  ( -31.99999999999999289, 29.99999999999997868, 5.000000000000004441 ) ) ;
#7906=CARTESIAN_POINT ( 'NONE',  ( 0.000000000000000000, 35.00000000000000000, 50.50000000000000000 ) ) ;
#7911=EDGE_CURVE ( 'NONE', #9473, #7366, #4206, .T. ) ;
#7912=VERTEX_POINT ( 'NONE', #3436 ) ;
#7929=CARTESIAN_POINT ( 'NONE',  ( 18.50000000000001776, 2.265596578422605368E-15, 0.000000000000000000 ) ) ;
#7930=VECTOR ( 'NONE', #7936, 1000.000000000000114 ) ;
#7936=DIRECTION ( 'NONE',  ( -0.7071067811865461294, 0.7071067811865489050, -3.960316634274389414E-15 ) ) ;
#7941=FACE_OUTER_BOUND ( 'NONE', #2041, .T. ) ;
#7950=AXIS2_PLACEMENT_3D ( 'NONE', #5329, #7480, #8061 ) ;
#7978=ORIENTED_EDGE ( 'NONE', *, *, #8930, .T. ) ;
#7983=FACE_OUTER_BOUND ( 'NONE', #6674, .T. ) ;
#7985=VECTOR ( 'NONE', #5892, 1000.000000000000114 ) ;
#7986=ORIENTED_EDGE ( 'NONE', *, *, #6576, .F. ) ;
#7995=EDGE_CURVE ( 'NONE', #8566, #1694, #6662, .T. ) ;
#8003=CARTESIAN_POINT ( 'NONE',  ( 0.000000000000000000, -17.50000000000000000, 49.50000000000000000 ) ) ;
#8007=CARTESIAN_POINT ( 'NONE',  ( -19.62310601229373574, -19.62310601229373574, 26.87436867076458924 ) ) ;
#8019=VECTOR ( 'NONE', #1662, 1000.000000000000000 ) ;
#8036=LINE ( 'NONE', #737, #8242 ) ;
#8061=DIRECTION ( 'NONE',  ( 1.000000000000000000, 0.000000000000000000, 0.000000000000000000 ) ) ;
#8067=PRODUCT_DEFINITION_FORMATION_WITH_SPECIFIED_SOURCE ( 'ANY', '', #4471, .NOT_KNOWN. ) ;
#8093=VECTOR ( 'NONE', #1, 1000.000000000000114 ) ;
#8104=VECTOR ( 'NONE', #3928, 1000.000000000000114 ) ;
#8119=VECTOR ( 'NONE', #4443, 1000.000000000000000 ) ;
#8137=ORIENTED_EDGE ( 'NONE', *, *, #4261, .F. ) ;
#8141=DIRECTION ( 'NONE',  ( 0.000000000000000000, -1.000000000000000000, 0.000000000000000000 ) ) ;
#8142=CARTESIAN_POINT ( 'NONE',  ( -17.49999999999999645, 4.703319286132084720, 49.50000000000000000 ) ) ;
#8161=PRODUCT_DEFINITION_SHAPE ( 'NONE', 'NONE',  #7762 ) ;
#8162=EDGE_CURVE ( 'NONE', #8254, #9088, #9450, .T. ) ;
#8171=DIRECTION ( 'NONE',  ( -1.000000000000000000, 0.000000000000000000, 0.000000000000000000 ) ) ;
#8179=ORIENTED_EDGE ( 'NONE', *, *, #7667, .T. ) ;
#8185=CARTESIAN_POINT ( 'NONE',  ( -17.50000000000000355, 2.143131898507868643E-15, 49.50000000000000000 ) ) ;
#8188=AXIS2_PLACEMENT_3D ( 'NONE', #8442, #4199, #4112 ) ;
#8189=VERTEX_POINT ( 'NONE', #1120 ) ;
#8197=CARTESIAN_POINT ( 'NONE',  ( 12.37436867076458036, 12.37436867076458036, 19.62563132923542142 ) ) ;
#8206=DIRECTION ( 'NONE',  ( -0.7071067811865455743, -1.057629477510965448E-15, 0.7071067811865493491 ) ) ;
#8228=CARTESIAN_POINT ( 'NONE',  ( 17.50000000000000355, 0.000000000000000000, 0.000000000000000000 ) ) ;
#8242=VECTOR ( 'NONE', #3761, 1000.000000000000000 ) ;
#8246=CARTESIAN_POINT ( 'NONE',  ( 2.143131898507868248E-15, -17.50000000000000000, 14.49999999999999822 ) ) ;
#8247=ADVANCED_FACE ( 'NONE', ( #981 ), #6865, .F. ) ;
#8254=VERTEX_POINT ( 'NONE', #4915 ) ;
#8255=DIRECTION ( 'NONE',  ( 0.000000000000000000, 0.000000000000000000, -1.000000000000000000 ) ) ;
#8256=EDGE_LOOP ( 'NONE', ( #3474, #4080, #2020, #9149 ) ) ;
#8257=EDGE_CURVE ( 'NONE', #5235, #3097, #4196, .T. ) ;
#8281=FACE_OUTER_BOUND ( 'NONE', #3168, .T. ) ;
#8285=EDGE_LOOP ( 'NONE', ( #5566, #1924, #7317, #7458, #2764, #52 ) ) ;
#8290=EDGE_CURVE ( 'NONE', #6850, #31, #8664, .T. ) ;
#8291=PLANE ( 'NONE',  #7372 ) ;
#8292=DIRECTION ( 'NONE',  ( -1.000000000000000000, 0.000000000000000000, -0.000000000000000000 ) ) ;
#8299=EDGE_CURVE ( 'NONE', #4913, #2936, #1005, .T. ) ;
#8312=PLANE ( 'NONE',  #7126 ) ;
#8317=ORIENTED_EDGE ( 'NONE', *, *, #2191, .F. ) ;
#8318=CARTESIAN_POINT ( 'NONE',  ( -31.99999999999999289, -34.99999999999999289, 5.000000000000004441 ) ) ;
#8326=EDGE_CURVE ( 'NONE', #7366, #6094, #9380, .T. ) ;
#8333=DIRECTION ( 'NONE',  ( 0.000000000000000000, 0.000000000000000000, -1.000000000000000000 ) ) ;
#8338=EDGE_LOOP ( 'NONE', ( #6210, #8466, #3612, #7047, #6610, #4807 ) ) ;
#8342=CARTESIAN_POINT ( 'NONE',  ( 0.000000000000000000, 34.00000000000001421, 32.00000000000000000 ) ) ;
#8360=CARTESIAN_POINT ( 'NONE',  ( 27.00000000000000355, 35.00000000000000000, 64.00000000000000000 ) ) ;
#8365=EDGE_CURVE ( 'NONE', #1286, #6850, #5937, .T. ) ;
#8369=EDGE_CURVE ( 'NONE', #2908, #7012, #8036, .T. ) ;
#8374=DIRECTION ( 'NONE',  ( -1.000000000000000000, 0.000000000000000000, 0.000000000000000000 ) ) ;
#8380=ORIENTED_EDGE ( 'NONE', *, *, #2177, .F. ) ;
#8393=AXIS2_PLACEMENT_3D ( 'NONE', #5833, #1452, #4481 ) ;
#8395=FACE_OUTER_BOUND ( 'NONE', #8256, .T. ) ;
#8403=VECTOR ( 'NONE', #7288, 999.9999999999998863 ) ;
#8410=CARTESIAN_POINT ( 'NONE',  ( 32.00000000000000711, 2.265596578422603791E-15, 50.50000000000000000 ) ) ;
#8415=FACE_OUTER_BOUND ( 'NONE', #7461, .T. ) ;
#8417=CARTESIAN_POINT ( 'NONE',  ( 2.143131898507868248E-15, -35.00000000000000000, 14.49999999999999822 ) ) ;
#8419=ORIENTED_EDGE ( 'NONE', *, *, #1838, .F. ) ;
#8423=ORIENTED_EDGE ( 'NONE', *, *, #4261, .T. ) ;
#8427=CARTESIAN_POINT ( 'NONE',  ( 17.50000000000000355, 0.000000000000000000, 1.000000000000021760 ) ) ;
#8433=EDGE_LOOP ( 'NONE', ( #4279, #8997, #6313 ) ) ;
#8438=EDGE_CURVE ( 'NONE', #8254, #7899, #4385, .T. ) ;
#8440=FACE_OUTER_BOUND ( 'NONE', #6954, .T. ) ;
#8442=CARTESIAN_POINT ( 'NONE',  ( 0.000000000000000000, 0.000000000000000000, 63.00000000000002842 ) ) ;
#8446=LINE ( 'NONE', #4604, #6252 ) ;
#8447=ORIENTED_EDGE ( 'NONE', *, *, #8290, .T. ) ;
#8453=AXIS2_PLACEMENT_3D ( 'NONE', #2867, #1923, #5759 ) ;
#8459=VECTOR ( 'NONE', #5460, 1000.000000000000000 ) ;
#8463=DIRECTION ( 'NONE',  ( -0.7071067811865494601, 0.7071067811865455743, 0.000000000000000000 ) ) ;
#8466=ORIENTED_EDGE ( 'NONE', *, *, #1731, .T. ) ;
#8468=CONICAL_SURFACE ( 'NONE', #3093, 17.50000000000000355, 0.7853981633974533860 ) ;
#8470=DIRECTION ( 'NONE',  ( 0.000000000000000000, 0.000000000000000000, 1.000000000000000000 ) ) ;
#8483=DIRECTION ( 'NONE',  ( 0.000000000000000000, 1.000000000000000000, 0.000000000000000000 ) ) ;
#8487=ORIENTED_EDGE ( 'NONE', *, *, #3230, .F. ) ;
#8496=AXIS2_PLACEMENT_3D ( 'NONE', #5020, #4967, #7177 ) ;
#8513=ADVANCED_FACE ( 'NONE', ( #4726 ), #8843, .F. ) ;
#8514=DIRECTION ( 'NONE',  ( -0.7071067811865525687, 0.000000000000000000, 0.7071067811865425767 ) ) ;
#8524=ADVANCED_FACE ( 'NONE', ( #6983 ), #5400, .F. ) ;
#8532=VERTEX_POINT ( 'NONE', #3185 ) ;
#8536=DIRECTION ( 'NONE',  ( -3.969829082701935600E-15, -0.7071067811865493491, 0.7071067811865456854 ) ) ;
#8539=VECTOR ( 'NONE', #2731, 1000.000000000000000 ) ;
#8540=FACE_OUTER_BOUND ( 'NONE', #254, .T. ) ;
#8545=VECTOR ( 'NONE', #4293, 1000.000000000000000 ) ;
#8547=ORIENTED_EDGE ( 'NONE', *, *, #5830, .T. ) ;
#8552=AXIS2_PLACEMENT_3D ( 'NONE', #2017, #1922, #9363 ) ;
#8559=AXIS2_PLACEMENT_3D ( 'NONE', #8342, #2539, #4700 ) ;
#8566=VERTEX_POINT ( 'NONE', #8427 ) ;
#8567=ORIENTED_EDGE ( 'NONE', *, *, #4548, .T. ) ;
#8577=CARTESIAN_POINT ( 'NONE',  ( 27.00000000000000355, -29.99999999999999289, 64.00000000000000000 ) ) ;
#8584=CARTESIAN_POINT ( 'NONE',  ( 32.00000000000000711, 35.00000000000000000, 5.000000000000031974 ) ) ;
#8592=CARTESIAN_POINT ( 'NONE',  ( -31.99999999999999289, 2.265596578422605368E-15, 13.49999999999998401 ) ) ;
#8593=CARTESIAN_POINT ( 'NONE',  ( 32.00000000000000711, -34.99999999999999289, 5.000000000000031974 ) ) ;
#8595=CARTESIAN_POINT ( 'NONE',  ( -26.99999999999998934, -34.99999999999999289, 58.99999999999997158 ) ) ;
#8596=ORIENTED_EDGE ( 'NONE', *, *, #3296, .T. ) ;
#8606=DIRECTION ( 'NONE',  ( 0.000000000000000000, 0.7071067811865494601, -0.7071067811865455743 ) ) ;
#8615=LINE ( 'NONE', #5699, #8907 ) ;
#8624=FACE_OUTER_BOUND ( 'NONE', #797, .T. ) ;
#8625=CARTESIAN_POINT ( 'NONE',  ( -29.49999999999998224, 29.99999999999997513, 2.500000000000006661 ) ) ;
#8627=DIRECTION ( 'NONE',  ( -1.000000000000000000, 0.000000000000000000, -0.000000000000000000 ) ) ;
#8638=LINE ( 'NONE', #8592, #8403 ) ;
#8660=FACE_OUTER_BOUND ( 'NONE', #5363, .T. ) ;
#8661=AXIS2_PLACEMENT_3D ( 'NONE', #2958, #5374, #8292 ) ;
#8664=LINE ( 'NONE', #7171, #3011 ) ;
#8673=ORIENTED_EDGE ( 'NONE', *, *, #6156, .F. ) ;
#8679=CARTESIAN_POINT ( 'NONE',  ( -26.99999999999998934, 35.00000000000000000, 5.000000000000004441 ) ) ;
#8681=ORIENTED_EDGE ( 'NONE', *, *, #3957, .F. ) ;
#8694=ORIENTED_EDGE ( 'NONE', *, *, #4314, .T. ) ;
#8699=DIRECTION ( 'NONE',  ( -0.000000000000000000, -0.000000000000000000, 1.000000000000000000 ) ) ;
#8700=CIRCLE ( 'NONE', #3955, 18.49999999999997513 ) ;
#8706=DIRECTION ( 'NONE',  ( -0.7071067811865456854, -3.969829082701935600E-15, 0.7071067811865493491 ) ) ;
#8707=VECTOR ( 'NONE', #1138, 1000.000000000000000 ) ;
#8712=CARTESIAN_POINT ( 'NONE',  ( 19.62310601229373574, -19.62310601229373574, 37.12563132923541787 ) ) ;
#8729=DIRECTION ( 'NONE',  ( 0.000000000000000000, 0.000000000000000000, -1.000000000000000000 ) ) ;
#8733=ORIENTED_EDGE ( 'NONE', *, *, #5557, .F. ) ;
#8740=ORIENTED_EDGE ( 'NONE', *, *, #1095, .F. ) ;
#8745=LINE ( 'NONE', #57, #5777 ) ;
#8746=CARTESIAN_POINT ( 'NONE',  ( -31.99999999999999289, 29.99999999999997868, 64.00000000000000000 ) ) ;
#8768=DIRECTION ( 'NONE',  ( 1.000000000000000000, 0.000000000000000000, 0.000000000000000000 ) ) ;
#8774=DIRECTION ( 'NONE',  ( 3.969829082701938755E-15, -0.7071067811865493491, -0.7071067811865455743 ) ) ;
#8775=CARTESIAN_POINT ( 'NONE',  ( 2.143131898507868248E-15, -17.50000000000000000, 14.49999999999999822 ) ) ;
#8777=ORIENTED_EDGE ( 'NONE', *, *, #1720, .T. ) ;
#8779=CARTESIAN_POINT ( 'NONE',  ( 17.50000000000000355, 0.000000000000000000, 49.50000000000000000 ) ) ;
#8795=VERTEX_POINT ( 'NONE', #7929 ) ;
#8796=CARTESIAN_POINT ( 'NONE',  ( 18.49999999999997513, 0.000000000000000000, 64.00000000000000000 ) ) ;
#8797=VERTEX_POINT ( 'NONE', #6315 ) ;
#8808=CARTESIAN_POINT ( 'NONE',  ( 0.000000000000000000, 34.00000000000001421, 49.50000000000000000 ) ) ;
#8810=VECTOR ( 'NONE', #8774, 1000.000000000000114 ) ;
#8811=PLANE ( 'NONE',  #4740 ) ;
#8814=VECTOR ( 'NONE', #1238, 1000.000000000000000 ) ;
#8819=CARTESIAN_POINT ( 'NONE',  ( -31.99999999999999289, -29.99999999999996447, 64.00000000000000000 ) ) ;
#8822=ORIENTED_EDGE ( 'NONE', *, *, #3400, .T. ) ;
#8823=CARTESIAN_POINT ( 'NONE',  ( 0.000000000000000000, 35.00000000000000000, 32.00000000000000000 ) ) ;
#8827=EDGE_CURVE ( 'NONE', #1163, #7881, #99, .T. ) ;
#8835=DIRECTION ( 'NONE',  ( 0.7071067811865456854, 0.7071067811865493491, -0.000000000000000000 ) ) ;
#8843=CONICAL_SURFACE ( 'NONE', #5482, 17.50000000000000355, 0.7853981633974466137 ) ;
#8853=CIRCLE ( 'NONE', #7324, 17.50000000000000355 ) ;
#8855=VECTOR ( 'NONE', #4549, 1000.000000000000114 ) ;
#8867=LINE ( 'NONE', #40, #7985 ) ;
#8887=DIRECTION ( 'NONE',  ( -1.000000000000000000, 0.000000000000000000, 0.000000000000000000 ) ) ;
#8888=DIRECTION ( 'NONE',  ( 0.000000000000000000, 0.000000000000000000, -1.000000000000000000 ) ) ;
#8890=DIRECTION ( 'NONE',  ( 1.000000000000000000, 0.000000000000000000, 0.000000000000000000 ) ) ;
#8891=DIRECTION ( 'NONE',  ( 0.000000000000000000, 1.000000000000000000, 0.000000000000000000 ) ) ;
#8897=DIRECTION ( 'NONE',  ( 0.000000000000000000, 0.7071067811865426878, 0.7071067811865524577 ) ) ;
#8906=DIRECTION ( 'NONE',  ( 0.000000000000000000, 1.000000000000000000, 0.000000000000000000 ) ) ;
#8907=VECTOR ( 'NONE', #4918, 1000.000000000000000 ) ;
#8917=( BOUNDED_CURVE ( )  B_SPLINE_CURVE ( 3, ( #5177, #4408, #1676, #8779 ),
 .UNSPECIFIED., .F., .T. ) 
 B_SPLINE_CURVE_WITH_KNOTS ( ( 4, 4 ),
 ( 5.497787143782137953, 6.283185307179586232 ),
 .UNSPECIFIED. ) 
 CURVE ( )  GEOMETRIC_REPRESENTATION_ITEM ( )  RATIONAL_B_SPLINE_CURVE ( ( 1.000000000000000000, 0.9492530216741911220, 0.9492530216741911220, 1.000000000000000000 ) ) 
 REPRESENTATION_ITEM ( '' )  );
#8919=ORIENTED_EDGE ( 'NONE', *, *, #1418, .F. ) ;
#8926=FACE_OUTER_BOUND ( 'NONE', #6097, .T. ) ;
#8928=ORIENTED_EDGE ( 'NONE', *, *, #5557, .T. ) ;
#8930=EDGE_CURVE ( 'NONE', #6850, #1286, #8853, .T. ) ;
#8935=EDGE_CURVE ( 'NONE', #9218, #8795, #6268, .T. ) ;
#8947=EDGE_CURVE ( 'NONE', #8797, #8189, #6596, .T. ) ;
#8954=ORIENTED_EDGE ( 'NONE', *, *, #8935, .T. ) ;
#8955=EDGE_LOOP ( 'NONE', ( #7488, #1570, #2358, #5597 ) ) ;
#8956=ORIENTED_EDGE ( 'NONE', *, *, #9357, .F. ) ;
#8957=FACE_OUTER_BOUND ( 'NONE', #8433, .T. ) ;
#8973=CARTESIAN_POINT ( 'NONE',  ( 27.00000000000000355, -29.99999999999999289, 64.00000000000000000 ) ) ;
#8978=LINE ( 'NONE', #5345, #3645 ) ;
#8983=VERTEX_POINT ( 'NONE', #8410 ) ;
#8989=DIRECTION ( 'NONE',  ( -0.000000000000000000, 1.000000000000000000, 0.000000000000000000 ) ) ;
#8991=FACE_BOUND ( 'NONE', #3404, .T. ) ;
#8997=ORIENTED_EDGE ( 'NONE', *, *, #608, .T. ) ;
#9001=CARTESIAN_POINT ( 'NONE',  ( 27.00000000000000355, 29.99999999999997158, 0.000000000000000000 ) ) ;
#9006=AXIS2_PLACEMENT_3D ( 'NONE', #5781, #8606, #5005 ) ;
#9008=AXIS2_PLACEMENT_3D ( 'NONE', #8595, #4278, #7018 ) ;
#9009=CARTESIAN_POINT ( 'NONE',  ( -29.49999999999999289, -29.99999999999997868, 61.49999999999998579 ) ) ;
#9014=ORIENTED_EDGE ( 'NONE', *, *, #3726, .T. ) ;
#9015=DIRECTION ( 'NONE',  ( -1.000000000000000000, -0.000000000000000000, -0.000000000000000000 ) ) ;
#9035=CARTESIAN_POINT ( 'NONE',  ( -12.37436867076458036, 12.37436867076458036, 44.37436867076458213 ) ) ;
#9040=LINE ( 'NONE', #5399, #2181 ) ;
#9042=CARTESIAN_POINT ( 'NONE',  ( 12.37436867076458036, 12.37436867076458036, 19.62563132923542142 ) ) ;
#9043=DIRECTION ( 'NONE',  ( -0.000000000000000000, -0.000000000000000000, -1.000000000000000000 ) ) ;
#9045=ORIENTED_EDGE ( 'NONE', *, *, #535, .T. ) ;
#9052=EDGE_CURVE ( 'NONE', #7912, #4290, #2616, .T. ) ;
#9060=ORIENTED_EDGE ( 'NONE', *, *, #5714, .T. ) ;
#9062=CIRCLE ( 'NONE', #4917, 18.50000000000000355 ) ;
#9067=CARTESIAN_POINT ( 'NONE',  ( 27.00000000000000355, 29.99999999999997158, 64.00000000000000000 ) ) ;
#9071=ORIENTED_EDGE ( 'NONE', *, *, #8827, .F. ) ;
#9088=VERTEX_POINT ( 'NONE', #3940 ) ;
#9102=ORIENTED_EDGE ( 'NONE', *, *, #4663, .F. ) ;
#9104=EDGE_LOOP ( 'NONE', ( #4489, #8547, #2043, #1052, #4370, #461, #7978 ) ) ;
#9105=EDGE_CURVE ( 'NONE', #3433, #2908, #8978, .T. ) ;
#9109=ADVANCED_FACE ( 'NONE', ( #296 ), #7640, .F. ) ;
#9119=DIRECTION ( 'NONE',  ( -0.000000000000000000, -0.7071067811865455743, -0.7071067811865494601 ) ) ;
#9120=VECTOR ( 'NONE', #3996, 1000.000000000000000 ) ;
#9143=CARTESIAN_POINT ( 'NONE',  ( 31.00000000000002132, 0.000000000000000000, 32.00000000000000000 ) ) ;
#9145=CARTESIAN_POINT ( 'NONE',  ( 0.000000000000000000, -34.99999999999999289, 32.00000000000000000 ) ) ;
#9149=ORIENTED_EDGE ( 'NONE', *, *, #4548, .F. ) ;
#9152=LINE ( 'NONE', #5382, #9170 ) ;
#9157=VECTOR ( 'NONE', #4407, 1000.000000000000000 ) ;
#9162=ORIENTED_EDGE ( 'NONE', *, *, #6896, .T. ) ;
#9169=EDGE_CURVE ( 'NONE', #9251, #8566, #3035, .T. ) ;
#9170=VECTOR ( 'NONE', #6100, 1000.000000000000000 ) ;
#9180=CARTESIAN_POINT ( 'NONE',  ( -31.99999999999999289, 35.00000000000000000, 64.00000000000000000 ) ) ;
#9185=AXIS2_PLACEMENT_3D ( 'NONE', #5533, #5439, #1779 ) ;
#9190=CARTESIAN_POINT ( 'NONE',  ( 0.000000000000000000, -34.00000000000001421, 32.00000000000000000 ) ) ;
#9201=CARTESIAN_POINT ( 'NONE',  ( 18.50000000000001776, 2.265596578422605368E-15, 0.000000000000000000 ) ) ;
#9206=ORIENTED_EDGE ( 'NONE', *, *, #8290, .F. ) ;
#9216=EDGE_CURVE ( 'NONE', #3965, #8532, #2583, .T. ) ;
#9217=( BOUNDED_CURVE ( )  B_SPLINE_CURVE ( 3, ( #3149, #7712, #6989, #4017 ),
 .UNSPECIFIED., .F., .T. ) 
 B_SPLINE_CURVE_WITH_KNOTS ( ( 4, 4 ),
 ( 3.141592653589793116, 3.926990816987241395 ),
 .UNSPECIFIED. ) 
 CURVE ( )  GEOMETRIC_REPRESENTATION_ITEM ( )  RATIONAL_B_SPLINE_CURVE ( ( 1.000000000000000000, 0.9492530216741911220, 0.9492530216741911220, 1.000000000000000000 ) ) 
 REPRESENTATION_ITEM ( '' )  );
#9218=VERTEX_POINT ( 'NONE', #6862 ) ;
#9220=DIRECTION ( 'NONE',  ( 0.000000000000000000, 0.000000000000000000, -1.000000000000000000 ) ) ;
#9236=CARTESIAN_POINT ( 'NONE',  ( -31.99999999999999289, 35.00000000000000000, 5.000000000000004441 ) ) ;
#9237=LINE ( 'NONE', #2039, #2061 ) ;
#9240=EDGE_LOOP ( 'NONE', ( #6659, #7237, #378, #2066, #6813, #7462 ) ) ;
#9247=CARTESIAN_POINT ( 'NONE',  ( -26.99999999999998934, 0.000000000000000000, 64.00000000000000000 ) ) ;
#9250=CARTESIAN_POINT ( 'NONE',  ( 12.37436867076458036, -12.37436867076458036, 44.37436867076458213 ) ) ;
#9251=VERTEX_POINT ( 'NONE', #4649 ) ;
#9268=LINE ( 'NONE', #2119, #5529 ) ;
#9287=EDGE_CURVE ( 'NONE', #6094, #1673, #8446, .T. ) ;
#9304=CARTESIAN_POINT ( 'NONE',  ( 2.143131898507868248E-15, 34.00000000000001421, 14.49999999999999822 ) ) ;
#9305=VECTOR ( 'NONE', #3202, 1000.000000000000000 ) ;
#9331=CARTESIAN_POINT ( 'NONE',  ( -17.49999999999999645, -4.703319286132082944, 14.49999999999999822 ) ) ;
#9334=VECTOR ( 'NONE', #169, 1000.000000000000000 ) ;
#9344=DIRECTION ( 'NONE',  ( 0.000000000000000000, 0.7071067811865493491, 0.7071067811865455743 ) ) ;
#9350=AXIS2_PLACEMENT_3D ( 'NONE', #4516, #8888, #8171 ) ;
#9352=CARTESIAN_POINT ( 'NONE',  ( 4.703319286132082944, -17.49999999999999645, 49.50000000000000000 ) ) ;
#9354=ORIENTED_EDGE ( 'NONE', *, *, #4006, .F. ) ;
#9357=EDGE_CURVE ( 'NONE', #3807, #2599, #3526, .T. ) ;
#9360=DIRECTION ( 'NONE',  ( 0.7071067811865494601, 0.000000000000000000, -0.7071067811865455743 ) ) ;
#9363=DIRECTION ( 'NONE',  ( 0.000000000000000000, 0.000000000000000000, 1.000000000000000000 ) ) ;
#9375=ORIENTED_EDGE ( 'NONE', *, *, #5104, .F. ) ;
#9376=CARTESIAN_POINT ( 'NONE',  ( -17.50000000000000355, 2.143131898507868643E-15, 14.49999999999999822 ) ) ;
#9378=AXIS2_PLACEMENT_3D ( 'NONE', #3812, #6755, #4585 ) ;
#9380=LINE ( 'NONE', #593, #4236 ) ;
#9392=LINE ( 'NONE', #8625, #5354 ) ;
#9398=DIRECTION ( 'NONE',  ( -0.000000000000000000, -0.000000000000000000, 1.000000000000000000 ) ) ;
#9401=ORIENTED_EDGE ( 'NONE', *, *, #5536, .T. ) ;
#9415=CONICAL_SURFACE ( 'NONE', #4362, 18.49999999999998934, 0.7853981633974517207 ) ;
#9422=DIRECTION ( 'NONE',  ( 0.7071067811865455743, 9.614813431917869865E-16, 0.7071067811865493491 ) ) ;
#9440=DIRECTION ( 'NONE',  ( 0.000000000000000000, -0.7071067811865456854, -0.7071067811865493491 ) ) ;
#9450=CIRCLE ( 'NONE', #861, 17.50000000000000000 ) ;
#9451=VECTOR ( 'NONE', #2815, 1000.000000000000000 ) ;
#9458=AXIS2_PLACEMENT_3D ( 'NONE', #5059, #1498, #5741 ) ;
#9470=VECTOR ( 'NONE', #1584, 1000.000000000000000 ) ;
#9471=LINE ( 'NONE', #2849, #3326 ) ;
#9473=VERTEX_POINT ( 'NONE', #3676 ) ;
#9509=COLOUR_RGB('Light Blue',0.38,0.62,0.78);
#9510=FILL_AREA_STYLE_COLOUR('',#9509);
#9511=FILL_AREA_STYLE('',(#9510));
#9512=SURFACE_STYLE_FILL_AREA(#9511);
#9513=SURFACE_SIDE_STYLE('',(#9512));
#9514=SURFACE_STYLE_USAGE(.BOTH.,#9513);
#9515=PRESENTATION_STYLE_ASSIGNMENT((#9514));
ENDSEC;
END-ISO-10303-21;
